ISO-10303-21;
HEADER;
FILE_DESCRIPTION (('STEP AP214'),
    '1' );
FILE_NAME ('torque nut 04-2_iso_ISO 7043-M6-N.step',
    '2026-09-21T15:58:29',
    ( '' ),
    ( '' ),
    'SwSTEP 2.0',
    'SolidWorks 2026',
    '' );
FILE_SCHEMA (( 'AUTOMOTIVE_DESIGN' ));
ENDSEC;

DATA;
#16=CARTESIAN_POINT ( 'NONE',  ( 4.999999999999997335, 0.000000000000000000, 0.000000000000000000 ) ) ;
#18=EDGE_LOOP ( 'NONE', ( #28205, #32238, #16851 ) ) ;
#91=CARTESIAN_POINT ( 'NONE',  ( 0.000000000000000000, 0.000000000000000000, -4.599999999999999645 ) ) ;
#141=CARTESIAN_POINT ( 'NONE',  ( -5.000000000000000888, 3.082654106983011122, -4.288941049016753659 ) ) ;
#143=ORIENTED_EDGE ( 'NONE', *, *, #17525, .F. ) ;
#197=CARTESIAN_POINT ( 'NONE',  ( 0.000000000000000000, 0.000000000000000000, 13.31572692736085095 ) ) ;
#276=ORIENTED_EDGE ( 'NONE', *, *, #16312, .T. ) ;
#278=CARTESIAN_POINT ( 'NONE',  ( 3.057313426867659167, 4.281874658697558900, -4.057628883416042775 ) ) ;
#280=B_SPLINE_CURVE_WITH_KNOTS ( 'NONE', 3,
 ( #34801, #31774, #15096, #20918, #14722, #278, #26525, #21088, #35175, #6104 ),
 .UNSPECIFIED., .F., .F.,
 ( 4, 2, 2, 2, 4 ),
 ( 8.020416891258658357E-20, 0.001528561485809837349, 0.003057122971619673831, 0.004585684457429509663, 0.006114245943239347662 ),
 .UNSPECIFIED. ) ;
#285=( LENGTH_UNIT ( ) NAMED_UNIT ( * ) SI_UNIT ( .MILLI., .METRE. ) );
#292=FACE_OUTER_BOUND ( 'NONE', #26627, .T. ) ;
#423=DIRECTION ( 'NONE',  ( 0.8191520442889913545, 1.003171929053524254E-16, -0.5735764363510468256 ) ) ;
#428=ORIENTED_EDGE ( 'NONE', *, *, #23008, .T. ) ;
#488=PRODUCT_DEFINITION_SHAPE ( 'NONE', 'NONE',  #14827 ) ;
#505=CARTESIAN_POINT ( 'NONE',  ( 5.236872748402765509, 0.5087250997262705576, -4.057689166958450500 ) ) ;
#557=ORIENTED_EDGE ( 'NONE', *, *, #18007, .T. ) ;
#558=CARTESIAN_POINT ( 'NONE',  ( -2.500000000000022204, 4.330127018922177662, 0.000000000000000000 ) ) ;
#573=DIRECTION ( 'NONE',  ( 1.000000000000000000, 0.000000000000000000, 0.000000000000000000 ) ) ;
#579=DIRECTION ( 'NONE',  ( 1.000000000000000000, 0.000000000000000000, 0.000000000000000000 ) ) ;
#599=PLANE ( 'NONE',  #19659 ) ;
#620=CARTESIAN_POINT ( 'NONE',  ( -1.738521435313295838, 5.045405839192962816, -4.085926550512736455 ) ) ;
#626=CARTESIAN_POINT ( 'NONE',  ( 3.357433326862127476, -3.835087656846213555, -0.07080520455423547355 ) ) ;
#648=CARTESIAN_POINT ( 'NONE',  ( -5.000000000000001776, 2.092572385047308359, -4.100081683154419565 ) ) ;
#669=DIRECTION ( 'NONE',  ( 1.000000000000000000, 0.000000000000000000, 0.000000000000000000 ) ) ;
#737=FACE_BOUND ( 'NONE', #17060, .T. ) ;
#774=B_SPLINE_CURVE_WITH_KNOTS ( 'NONE', 3,
 ( #8176, #19617, #16816, #18875, #13614, #30843 ),
 .UNSPECIFIED., .F., .F.,
 ( 4, 2, 4 ),
 ( 0.000000000000000000, 0.0002514304509865738471, 0.0005028609019731476943 ),
 .UNSPECIFIED. ) ;
#777=CARTESIAN_POINT ( 'NONE',  ( 0.000000000000000000, 0.000000000000000000, 2.266666666666666607 ) ) ;
#782=CARTESIAN_POINT ( 'NONE',  ( -2.500000000000000444, 3.061616997868383634E-16, -5.700000000000000178 ) ) ;
#793=CARTESIAN_POINT ( 'NONE',  ( 4.191707736911197912, -3.353419101626359478, -0.2701150775514091773 ) ) ;
#834=LINE ( 'NONE', #21084, #6157 ) ;
#845=CARTESIAN_POINT ( 'NONE',  ( -6.069707180676227632E-15, 5.773502691896268857, -5.700000000000000178 ) ) ;
#855=EDGE_CURVE ( 'NONE', #30871, #2722, #28965, .T. ) ;
#882=CARTESIAN_POINT ( 'NONE',  ( 0.000000000000000000, 0.000000000000000000, -4.599999999999999645 ) ) ;
#888=ORIENTED_EDGE ( 'NONE', *, *, #23980, .F. ) ;
#893=CARTESIAN_POINT ( 'NONE',  ( -5.170224855064533998, -2.788471980053888188, -4.289066185948688492 ) ) ;
#895=B_SPLINE_CURVE_WITH_KNOTS ( 'NONE', 3,
 ( #8671, #10768, #25766, #37009, #36459, #33643 ),
 .UNSPECIFIED., .F., .F.,
 ( 4, 2, 4 ),
 ( 0.003058795990767219572, 0.004586520967003283183, 0.006114245943239346795 ),
 .UNSPECIFIED. ) ;
#916=ORIENTED_EDGE ( 'NONE', *, *, #2941, .T. ) ;
#980=DIRECTION ( 'NONE',  ( 0.000000000000000000, 0.000000000000000000, 1.000000000000000000 ) ) ;
#998=EDGE_CURVE ( 'NONE', #15802, #18239, #5937, .T. ) ;
#1000=VERTEX_POINT ( 'NONE', #25083 ) ;
#1011=DIRECTION ( 'NONE',  ( -0.000000000000000000, -0.000000000000000000, 1.000000000000000000 ) ) ;
#1073=ORIENTED_EDGE ( 'NONE', *, *, #23008, .F. ) ;
#1206=CIRCLE ( 'NONE', #22169, 0.5671001622691687061 ) ;
#1208=CARTESIAN_POINT ( 'NONE',  ( -4.999999999999538147, 1.069480574179262788, -3.973098401497047405 ) ) ;
#1263=DIRECTION ( 'NONE',  ( -1.000000000000000000, 0.000000000000000000, 0.000000000000000000 ) ) ;
#1285=CARTESIAN_POINT ( 'NONE',  ( -5.000000000000000888, 2.886751345948107783, -0.5999999999999836575 ) ) ;
#1323=AXIS2_PLACEMENT_3D ( 'NONE', #777, #20467, #6773 ) ;
#1374=LINE ( 'NONE', #29677, #35867 ) ;
#1375=CARTESIAN_POINT ( 'NONE',  ( 4.999999999999999112, 2.886751345948125991, -3.984345921091767551 ) ) ;
#1383=CIRCLE ( 'NONE', #21752, 4.999999999999997335 ) ;
#1430=DIRECTION ( 'NONE',  ( -0.000000000000000000, -0.000000000000000000, 1.000000000000000000 ) ) ;
#1523=LINE ( 'NONE', #27030, #20347 ) ;
#1556=ORIENTED_EDGE ( 'NONE', *, *, #15598, .T. ) ;
#1570=DIRECTION ( 'NONE',  ( -0.000000000000000000, -0.000000000000000000, 1.000000000000000000 ) ) ;
#1620=CARTESIAN_POINT ( 'NONE',  ( 5.000000000000000888, 0.000000000000000000, 13.31572692736085095 ) ) ;
#1631=VECTOR ( 'NONE', #33925, 1000.000000000000000 ) ;
#1651=ORIENTED_EDGE ( 'NONE', *, *, #32671, .F. ) ;
#1652=CIRCLE ( 'NONE', #23814, 3.750000000000001776 ) ;
#1701=DIRECTION ( 'NONE',  ( 1.000000000000000000, 0.000000000000000000, 0.000000000000000000 ) ) ;
#1727=CARTESIAN_POINT ( 'NONE',  ( 0.000000000000000000, 0.000000000000000000, -25.03750572909317285 ) ) ;
#1749=ORIENTED_EDGE ( 'NONE', *, *, #32760, .T. ) ;
#1789=ORIENTED_EDGE ( 'NONE', *, *, #19867, .T. ) ;
#1864=CARTESIAN_POINT ( 'NONE',  ( 2.068360682592127020, 4.579334095020458406, -0.01465562841807926259 ) ) ;
#1874=ORIENTED_EDGE ( 'NONE', *, *, #2305, .F. ) ;
#1917=CARTESIAN_POINT ( 'NONE',  ( 5.170224855064530445, -2.788471980053870869, -4.289066185948684939 ) ) ;
#1944=CARTESIAN_POINT ( 'NONE',  ( 4.999999999999999112, 2.886751345948125991, -5.700000000000000178 ) ) ;
#1970=CARTESIAN_POINT ( 'NONE',  ( 3.060208875726632805, -4.280211771583998903, -4.057749648769106265 ) ) ;
#2030=ORIENTED_EDGE ( 'NONE', *, *, #27739, .F. ) ;
#2034=FACE_OUTER_BOUND ( 'NONE', #21873, .T. ) ;
#2074=DIRECTION ( 'NONE',  ( -0.000000000000000000, -0.000000000000000000, 1.000000000000000000 ) ) ;
#2227=ADVANCED_FACE ( 'NONE', ( #29556 ), #18704, .F. ) ;
#2239=CARTESIAN_POINT ( 'NONE',  ( -6.069707180676227632E-15, 5.773502691896268857, -3.984345921091771547 ) ) ;
#2276=CARTESIAN_POINT ( 'NONE',  ( 2.500000000000002220, -4.330127018922225623, -3.620524600599886345 ) ) ;
#2278=CARTESIAN_POINT ( 'NONE',  ( 5.236973622080098423, -1.063218227091886625, -4.059287483237865146 ) ) ;
#2293=CARTESIAN_POINT ( 'NONE',  ( -0.1702248550645306668, -5.871782057790580822, -4.289066185948700038 ) ) ;
#2303=AXIS2_PLACEMENT_3D ( 'NONE', #10897, #19891, #36773 ) ;
#2305=EDGE_CURVE ( 'NONE', #8160, #3797, #2863, .T. ) ;
#2386=CIRCLE ( 'NONE', #13157, 2.500000000000000444 ) ;
#2387=CARTESIAN_POINT ( 'NONE',  ( 2.069940739436594068, -4.578421848776002889, -2.348737659441448779E-14 ) ) ;
#2464=CARTESIAN_POINT ( 'NONE',  ( -5.000000000000000888, 2.886751345948107783, -3.984345921091764886 ) ) ;
#2465=CARTESIAN_POINT ( 'NONE',  ( 5.244723176341855364, 2.047152853917212134, -4.175731492522787747 ) ) ;
#2479=CARTESIAN_POINT ( 'NONE',  ( -4.319324222803803792, 3.279739689143194248, -3.838711833383783745 ) ) ;
#2565=ORIENTED_EDGE ( 'NONE', *, *, #26001, .F. ) ;
#2599=LINE ( 'NONE', #11032, #1631 ) ;
#2610=EDGE_LOOP ( 'NONE', ( #3078, #11977, #36547, #276 ) ) ;
#2636=DIRECTION ( 'NONE',  ( 1.000000000000000000, 0.000000000000000000, 0.000000000000000000 ) ) ;
#2647=FACE_OUTER_BOUND ( 'NONE', #11058, .T. ) ;
#2689=CARTESIAN_POINT ( 'NONE',  ( -5.000000000000000888, -1.947799557644010582, -0.2684016432552386311 ) ) ;
#2702=ORIENTED_EDGE ( 'NONE', *, *, #10157, .T. ) ;
#2722=VERTEX_POINT ( 'NONE', #10590 ) ;
#2788=AXIS2_PLACEMENT_3D ( 'NONE', #197, #23080, #18393 ) ;
#2811=EDGE_CURVE ( 'NONE', #3797, #26674, #36138, .T. ) ;
#2821=ORIENTED_EDGE ( 'NONE', *, *, #20519, .T. ) ;
#2823=VECTOR ( 'NONE', #33795, 1000.000000000000000 ) ;
#2846=CONICAL_SURFACE ( 'NONE', #6416, 4.999999999999997335, 0.9110539511682894664 ) ;
#2858=ADVANCED_FACE ( 'NONE', ( #31204 ), #19965, .T. ) ;
#2863=CIRCLE ( 'NONE', #31587, 4.999999999999997335 ) ;
#2888=CARTESIAN_POINT ( 'NONE',  ( 4.999999999999999112, 2.886751345948125991, -3.984345921091767551 ) ) ;
#2941=EDGE_CURVE ( 'NONE', #26674, #34191, #1383, .T. ) ;
#2972=DIRECTION ( 'NONE',  ( -1.000000000000000000, 0.000000000000000000, 0.000000000000000000 ) ) ;
#2996=B_SPLINE_CURVE_WITH_KNOTS ( 'NONE', 3,
 ( #18780, #24974, #16169, #7344, #35659 ),
 .UNSPECIFIED., .F., .F.,
 ( 4, 1, 4 ),
 ( 0.000000000000000000, 0.002886751345948134623, 0.005773502691896269245 ),
 .UNSPECIFIED. ) ;
#3026=( BOUNDED_SURFACE ( )  B_SPLINE_SURFACE ( 3, 2, ( 
 ( #14412, #141, #11571 ),
 ( #34475, #648, #32327 ),
 ( #32125, #1208, #23519 ),
 ( #12439, #17697, #6645 ),
 ( #12628, #29137, #4216 ),
 ( #18074, #29885, #29326 ) ),
 .UNSPECIFIED., .F., .F., .T. ) 
 B_SPLINE_SURFACE_WITH_KNOTS ( ( 4, 2, 4 ),
 ( 3, 3 ),
 ( 0.02453827135564170051, 0.02760610364996546329, 0.03067393594428922607 ),
 ( 0.000000000000000000, 1.000000000000000000 ),
 .UNSPECIFIED. ) 
 GEOMETRIC_REPRESENTATION_ITEM ( )  RATIONAL_B_SPLINE_SURFACE ( (
 ( 1.000000000000000000, 0.8047780919262715882, 1.000000000000000000),
 ( 1.000000000000000000, 0.8123791475856069200, 1.000000000000000000),
 ( 1.000000000000000000, 0.8190679386130260697, 1.000000000000000000),
 ( 1.000000000000000000, 0.8192344721910548300, 1.000000000000000000),
 ( 1.000000000000000000, 0.8126125954010035013, 1.000000000000000000),
 ( 1.000000000000000000, 0.8047712666188978625, 1.000000000000000000) ) ) 
 REPRESENTATION_ITEM ( '' )  SURFACE ( )  );
#3047=CARTESIAN_POINT ( 'NONE',  ( 3.050000000000000711, 0.000000000000000000, 2.266666666666999674 ) ) ;
#3075=CARTESIAN_POINT ( 'NONE',  ( -0.8653900595644542504, 5.556556492855577289, -4.190801088233095051 ) ) ;
#3078=ORIENTED_EDGE ( 'NONE', *, *, #7785, .F. ) ;
#3094=CARTESIAN_POINT ( 'NONE',  ( 3.514986608498387177, 4.017641317389688993, -4.057689166958403426 ) ) ;
#3101=DIRECTION ( 'NONE',  ( 0.000000000000000000, 0.000000000000000000, 1.000000000000000000 ) ) ;
#3110=B_SPLINE_CURVE_WITH_KNOTS ( 'NONE', 3,
 ( #35453, #12720, #9927, #30555, #36727, #1864, #11027, #28104 ),
 .UNSPECIFIED., .F., .F.,
 ( 4, 2, 2, 4 ),
 ( 2.451332856840218572E-07, 0.001475502392055680302, 0.002213131021440678352, 0.002950759650825675751 ),
 .UNSPECIFIED. ) ;
#3119=( NAMED_UNIT ( * ) PLANE_ANGLE_UNIT ( ) SI_UNIT ( $, .RADIAN. ) );
#3125=ADVANCED_FACE ( 'NONE', ( #30773 ), #36093, .F. ) ;
#3186=LINE ( 'NONE', #20805, #36237 ) ;
#3218=VERTEX_POINT ( 'NONE', #33046 ) ;
#3250=CARTESIAN_POINT ( 'NONE',  ( 0.000000000000000000, 0.000000000000000000, 0.000000000000000000 ) ) ;
#3253=FACE_OUTER_BOUND ( 'NONE', #19160, .T. ) ;
#3262=DIRECTION ( 'NONE',  ( 0.000000000000000000, 0.000000000000000000, 1.000000000000000000 ) ) ;
#3291=SURFACE_STYLE_FILL_AREA ( #31782 ) ;
#3314=PLANE ( 'NONE',  #23956 ) ;
#3399=ADVANCED_FACE ( 'NONE', ( #27004 ), #22267, .T. ) ;
#3400=CARTESIAN_POINT ( 'NONE',  ( -4.999999999999997335, 0.000000000000000000, 0.000000000000000000 ) ) ;
#3443=CARTESIAN_POINT ( 'NONE',  ( 5.000000000000007994, -2.886751345948139758, -0.5999999999999998668 ) ) ;
#3488=CARTESIAN_POINT ( 'NONE',  ( 0.000000000000000000, 0.000000000000000000, 2.266666666666999674 ) ) ;
#3569=PLANE ( 'NONE',  #34638 ) ;
#3574=CARTESIAN_POINT ( 'NONE',  ( 0.000000000000000000, 0.000000000000000000, -4.599999999999999645 ) ) ;
#3617=LINE ( 'NONE', #782, #24566 ) ;
#3672=PRESENTATION_STYLE_ASSIGNMENT (( #20716 ) ) ;
#3687=CARTESIAN_POINT ( 'NONE',  ( 5.248984340851194474, 2.531668808681894145, -4.266868479993926044 ) ) ;
#3704=CARTESIAN_POINT ( 'NONE',  ( 0.000000000000000000, 0.000000000000000000, -4.599999999999999645 ) ) ;
#3797=VERTEX_POINT ( 'NONE', #19491 ) ;
#3812=EDGE_LOOP ( 'NONE', ( #18038, #12025, #16189, #35900 ) ) ;
#3816=CARTESIAN_POINT ( 'NONE',  ( 5.122341571230611734, 2.957385285031201239, -4.281776566113604687 ) ) ;
#3844=( GEOMETRIC_REPRESENTATION_CONTEXT ( 3 ) GLOBAL_UNCERTAINTY_ASSIGNED_CONTEXT ( ( #33178 ) ) GLOBAL_UNIT_ASSIGNED_CONTEXT ( ( #285, #3119, #34628 ) ) REPRESENTATION_CONTEXT ( 'NONE', 'WORKASPACE' ) );
#3881=CARTESIAN_POINT ( 'NONE',  ( 0.000000000000000000, 0.000000000000000000, -5.700000000000000178 ) ) ;
#3890=ORIENTED_EDGE ( 'NONE', *, *, #18021, .T. ) ;
#3900=ORIENTED_EDGE ( 'NONE', *, *, #12178, .F. ) ;
#3945=CARTESIAN_POINT ( 'NONE',  ( -2.500000000000000444, 3.061616997868383634E-16, 1.716666666667001406 ) ) ;
#3954=CIRCLE ( 'NONE', #21321, 4.999999999999997335 ) ;
#4054=CIRCLE ( 'NONE', #29174, 6.532899837730827386 ) ;
#4070=CARTESIAN_POINT ( 'NONE',  ( 0.000000000000000000, 0.000000000000000000, -5.700000000000000178 ) ) ;
#4128=DIRECTION ( 'NONE',  ( 1.000000000000000000, 0.000000000000000000, 0.000000000000000000 ) ) ;
#4132=FACE_OUTER_BOUND ( 'NONE', #5232, .T. ) ;
#4216=CARTESIAN_POINT ( 'NONE',  ( -5.244721985554689603, -2.047016837486758778, -4.175706277538008493 ) ) ;
#4237=ADVANCED_FACE ( 'NONE', ( #3253 ), #37078, .F. ) ;
#4261=CARTESIAN_POINT ( 'NONE',  ( 0.000000000000000000, 0.000000000000000000, -5.700000000000001066 ) ) ;
#4292=CARTESIAN_POINT ( 'NONE',  ( -2.714587707229022318, 4.206234748388728129, -1.833826330805560234E-16 ) ) ;
#4311=PLANE ( 'NONE',  #33829 ) ;
#4327=CARTESIAN_POINT ( 'NONE',  ( 0.000000000000000000, 0.000000000000000000, 0.000000000000000000 ) ) ;
#4346=FACE_OUTER_BOUND ( 'NONE', #21165, .T. ) ;
#4370=ADVANCED_FACE ( 'NONE', ( #6629 ), #26087, .T. ) ;
#4402=CARTESIAN_POINT ( 'NONE',  ( -3.050000000000000711, 3.735172737399428132E-16, 2.266666666666999674 ) ) ;
#4423=CARTESIAN_POINT ( 'NONE',  ( 4.654160418576254177E-15, -6.066067634115602125, -4.359491423763670603 ) ) ;
#4425=ORIENTED_EDGE ( 'NONE', *, *, #13336, .F. ) ;
#4430=B_SPLINE_CURVE_WITH_KNOTS ( 'NONE', 3,
 ( #30594, #31687, #34511, #11802, #28503, #9010, #6022, #17610, #31313, #34327 ),
 .UNSPECIFIED., .F., .F.,
 ( 4, 2, 2, 2, 4 ),
 ( 0.000000000000000000, 0.001528561485809837566, 0.003057122971619675132, 0.004585684457429513132, 0.006114245943239348530 ),
 .UNSPECIFIED. ) ;
#4455=ORIENTED_EDGE ( 'NONE', *, *, #17155, .T. ) ;
#4542=EDGE_LOOP ( 'NONE', ( #27961, #15819, #17588, #23536, #15718 ) ) ;
#4613=( GEOMETRIC_REPRESENTATION_CONTEXT ( 3 ) GLOBAL_UNCERTAINTY_ASSIGNED_CONTEXT ( ( #33935 ) ) GLOBAL_UNIT_ASSIGNED_CONTEXT ( ( #21900, #30699, #18724 ) ) REPRESENTATION_CONTEXT ( 'NONE', 'WORKASPACE' ) );
#4637=AXIS2_PLACEMENT_3D ( 'NONE', #34215, #25771, #17126 ) ;
#4660=CARTESIAN_POINT ( 'NONE',  ( -3.514986608498314347, -4.017641317389597511, -4.057689166958359905 ) ) ;
#4671=SURFACE_STYLE_FILL_AREA ( #13096 ) ;
#4683=ADVANCED_FACE ( 'NONE', ( #33992 ), #31453, .F. ) ;
#4690=CARTESIAN_POINT ( 'NONE',  ( -6.532899837730827386, 8.000494875427320504E-16, -5.132899837730832360 ) ) ;
#4697=CARTESIAN_POINT ( 'NONE',  ( -5.826918817341602493E-15, 5.807445019730648639, -4.151004066889659505 ) ) ;
#4855=VERTEX_POINT ( 'NONE', #3945 ) ;
#4893=APPLICATION_CONTEXT ( 'automotive_design' ) ;
#4920=CARTESIAN_POINT ( 'NONE',  ( 0.6806757771967111292, -5.380514348700923932, -3.838711833385402006 ) ) ;
#4974=CARTESIAN_POINT ( 'NONE',  ( 0.4318028594007650156, -5.811705888749012949, -4.266911319714234985 ) ) ;
#5000=DIRECTION ( 'NONE',  ( 1.000000000000000000, 0.000000000000000000, 0.000000000000000000 ) ) ;
#5041=EDGE_CURVE ( 'NONE', #16004, #34714, #15926, .T. ) ;
#5098=CARTESIAN_POINT ( 'NONE',  ( 3.401922400366974131, -3.809401878282419940, -3.971474537231029611 ) ) ;
#5112=CIRCLE ( 'NONE', #31435, 3.000000000000000888 ) ;
#5119=DIRECTION ( 'NONE',  ( -1.000000000000000000, 1.224646799147353700E-16, 0.000000000000000000 ) ) ;
#5153=VECTOR ( 'NONE', #36108, 1000.000000000000000 ) ;
#5194=CARTESIAN_POINT ( 'NONE',  ( 4.999999999999999112, -0.4954705650270037065, -1.356946781501389143E-15 ) ) ;
#5211=CARTESIAN_POINT ( 'NONE',  ( 4.296971609539972370, 3.292644976428022119, -4.096693167834859928 ) ) ;
#5232=EDGE_LOOP ( 'NONE', ( #24060, #23051 ) ) ;
#5268=EDGE_CURVE ( 'NONE', #1000, #35211, #7751, .T. ) ;
#5270=FACE_OUTER_BOUND ( 'NONE', #36473, .T. ) ;
#5301=CARTESIAN_POINT ( 'NONE',  ( -0.6806757771964039305, 5.380514348701066041, -3.838711833385082262 ) ) ;
#5302=CARTESIAN_POINT ( 'NONE',  ( 3.417629563432208251, -3.800333343458275781, -3.719399823475529665 ) ) ;
#5324=DIRECTION ( 'NONE',  ( 1.224646799147353207E-16, 1.000000000000000000, 0.000000000000000000 ) ) ;
#5330=DIRECTION ( 'NONE',  ( 0.000000000000000000, 0.000000000000000000, -1.000000000000000000 ) ) ;
#5346=ORIENTED_EDGE ( 'NONE', *, *, #24733, .T. ) ;
#5379=LINE ( 'NONE', #16815, #6501 ) ;
#5390=CARTESIAN_POINT ( 'NONE',  ( 4.999999999999999112, -2.426004080355343095, -0.4213009713786298738 ) ) ;
#5398=DIRECTION ( 'NONE',  ( -0.000000000000000000, -0.000000000000000000, 1.000000000000000000 ) ) ;
#5435=( BOUNDED_SURFACE ( )  B_SPLINE_SURFACE ( 3, 2, ( 
 ( #8625, #25714, #8281 ),
 ( #30759, #20059, #7903 ),
 ( #16522, #27953, #2278 ),
 ( #13713, #25170, #16722 ),
 ( #5464, #28147, #2465 ),
 ( #25332, #11068, #19712 ) ),
 .UNSPECIFIED., .F., .F., .T. ) 
 B_SPLINE_SURFACE_WITH_KNOTS ( ( 4, 2, 4 ),
 ( 3, 3 ),
 ( 0.02452952700623422036, 0.02759707648669815216, 0.03066462596716208050 ),
 ( 0.000000000000000000, 1.000000000000000000 ),
 .UNSPECIFIED. ) 
 GEOMETRIC_REPRESENTATION_ITEM ( )  RATIONAL_B_SPLINE_SURFACE ( (
 ( 1.000000000000000000, 0.8047781199190355839, 1.000000000000000000),
 ( 1.000000000000000000, 0.8123783328842254514, 1.000000000000000000),
 ( 1.000000000000000000, 0.8190665273150808945, 1.000000000000000000),
 ( 1.000000000000000000, 0.8192358268326377368, 1.000000000000000000),
 ( 1.000000000000000000, 0.8126132377674081253, 1.000000000000000000),
 ( 1.000000000000000000, 0.8047712443734141852, 1.000000000000000000) ) ) 
 REPRESENTATION_ITEM ( '' )  SURFACE ( )  );
#5464=CARTESIAN_POINT ( 'NONE',  ( 4.999999999999999112, 2.094490679362924546, -3.837546594561450863 ) ) ;
#5506=ADVANCED_FACE ( 'NONE', ( #26289 ), #599, .T. ) ;
#5515=EDGE_LOOP ( 'NONE', ( #34661, #27608, #7035, #21329 ) ) ;
#5719=DIRECTION ( 'NONE',  ( 1.000000000000000000, 0.000000000000000000, 0.000000000000000000 ) ) ;
#5756=B_SPLINE_CURVE_WITH_KNOTS ( 'NONE', 3,
 ( #26743, #3687, #23556, #23752, #505, #14746 ),
 .UNSPECIFIED., .F., .F.,
 ( 4, 2, 4 ),
 ( 0.000000000000000000, 0.001529397995383609786, 0.003058795990767219572 ),
 .UNSPECIFIED. ) ;
#5791=CARTESIAN_POINT ( 'NONE',  ( -3.352586340487482719, -3.837886065734386065, -0.05822226285685593722 ) ) ;
#5819=B_SPLINE_CURVE_WITH_KNOTS ( 'NONE', 3,
 ( #10636, #5390, #16825, #8554, #5194, #24886 ),
 .UNSPECIFIED., .F., .F.,
 ( 4, 2, 4 ),
 ( 0.004308305454211647581, 0.005784651566377423289, 0.007260997678543198997 ),
 .UNSPECIFIED. ) ;
#5901=AXIS2_PLACEMENT_3D ( 'NONE', #23907, #35359, #9647 ) ;
#5929=CARTESIAN_POINT ( 'NONE',  ( -5.236872748402766398, -0.5087250997262755536, -4.057689166958452276 ) ) ;
#5937=B_SPLINE_CURVE_WITH_KNOTS ( 'NONE', 3,
 ( #27507, #7633, #19626, #18879, #13250, #22075 ),
 .UNSPECIFIED., .F., .F.,
 ( 4, 2, 4 ),
 ( -3.988673288089476442E-06, 0.0002483701411510734502, 0.0005007289555902363692 ),
 .UNSPECIFIED. ) ;
#5969=CIRCLE ( 'NONE', #19149, 1.133333333332999571 ) ;
#5971=DIRECTION ( 'NONE',  ( -0.000000000000000000, -0.000000000000000000, 1.000000000000000000 ) ) ;
#6018=CARTESIAN_POINT ( 'NONE',  ( 4.654160418576254177E-15, -6.066067634115602125, -4.359491423763670603 ) ) ;
#6022=CARTESIAN_POINT ( 'NONE',  ( -3.500188911486801224, -4.028306647601615609, -4.085926550512745337 ) ) ;
#6043=EDGE_CURVE ( 'NONE', #23996, #3218, #4054, .T. ) ;
#6060=CARTESIAN_POINT ( 'NONE',  ( 5.000000000000000000, 1.924500897298748958, -3.818275046351161883 ) ) ;
#6070=DIRECTION ( 'NONE',  ( 0.000000000000000000, 0.000000000000000000, 1.000000000000000000 ) ) ;
#6104=CARTESIAN_POINT ( 'NONE',  ( 5.253368672218635460, 3.033033817057773529, -4.359491423763652840 ) ) ;
#6138=AXIS2_PLACEMENT_3D ( 'NONE', #4690, #24569, #10676 ) ;
#6139=EDGE_CURVE ( 'NONE', #24840, #32261, #32163, .T. ) ;
#6157=VECTOR ( 'NONE', #12640, 1000.000000000000000 ) ;
#6167=AXIS2_PLACEMENT_3D ( 'NONE', #17138, #6070, #17674 ) ;
#6198=B_SPLINE_CURVE_WITH_KNOTS ( 'NONE', 3,
 ( #36143, #7646, #19099, #35975, #18709, #13431, #10645, #30525 ),
 .UNSPECIFIED., .F., .F.,
 ( 4, 2, 2, 4 ),
 ( 0.007260997678543198997, 0.007995810154593248689, 0.008730622630643298382, 0.01020024758274339603 ),
 .UNSPECIFIED. ) ;
#6222=CARTESIAN_POINT ( 'NONE',  ( 2.499999999999998224, 4.330127018922196314, -3.620524600599877019 ) ) ;
#6259=FACE_OUTER_BOUND ( 'NONE', #28318, .T. ) ;
#6273=CARTESIAN_POINT ( 'NONE',  ( -6.069707180676227632E-15, 5.773502691896268857, -3.984345921091771547 ) ) ;
#6310=ORIENTED_EDGE ( 'NONE', *, *, #2305, .T. ) ;
#6416=AXIS2_PLACEMENT_3D ( 'NONE', #10407, #21847, #16410 ) ;
#6431=ORIENTED_EDGE ( 'NONE', *, *, #15358, .F. ) ;
#6501=VECTOR ( 'NONE', #19806, 1000.000000000000000 ) ;
#6608=CARTESIAN_POINT ( 'NONE',  ( -5.236872748402766398, -8.269757189038523917E-14, -4.057689166958448723 ) ) ;
#6629=FACE_OUTER_BOUND ( 'NONE', #29157, .T. ) ;
#6645=CARTESIAN_POINT ( 'NONE',  ( -5.236775518523551831, -1.021013561554246607, -4.056148586100849052 ) ) ;
#6647=ORIENTED_EDGE ( 'NONE', *, *, #16968, .F. ) ;
#6655=CARTESIAN_POINT ( 'NONE',  ( -5.000000000000000888, 2.886751345948107783, -3.984345921091764886 ) ) ;
#6662=DIRECTION ( 'NONE',  ( 1.000000000000000000, 0.000000000000000000, 0.000000000000000000 ) ) ;
#6762=CARTESIAN_POINT ( 'NONE',  ( 0.000000000000000000, 0.000000000000000000, 0.000000000000000000 ) ) ;
#6773=DIRECTION ( 'NONE',  ( 1.000000000000000000, 0.000000000000000000, 0.000000000000000000 ) ) ;
#6861=DIRECTION ( 'NONE',  ( 0.8660254037844360431, 0.5000000000000045519, 0.000000000000000000 ) ) ;
#6891=ADVANCED_FACE ( 'NONE', ( #19881 ), #29367, .T. ) ;
#6907=CARTESIAN_POINT ( 'NONE',  ( -4.598786737361987953, 3.118391931134617323, -0.4203182062997219970 ) ) ;
#6957=AXIS2_PLACEMENT_3D ( 'NONE', #28641, #5971, #2972 ) ;
#6983=VECTOR ( 'NONE', #423, 999.9999999999998863 ) ;
#7035=ORIENTED_EDGE ( 'NONE', *, *, #33845, .T. ) ;
#7128=CARTESIAN_POINT ( 'NONE',  ( 4.999999999999999112, 2.886751345948125991, -5.700000000000000178 ) ) ;
#7200=ORIENTED_EDGE ( 'NONE', *, *, #14594, .F. ) ;
#7265=DIRECTION ( 'NONE',  ( 0.000000000000000000, 0.000000000000000000, -1.000000000000000000 ) ) ;
#7280=CARTESIAN_POINT ( 'NONE',  ( 0.000000000000000000, 0.000000000000000000, -5.700000000000000178 ) ) ;
#7299=AXIS2_PLACEMENT_3D ( 'NONE', #30790, #10563, #24819 ) ;
#7337=EDGE_LOOP ( 'NONE', ( #33032, #18630, #10854, #7200 ) ) ;
#7344=CARTESIAN_POINT ( 'NONE',  ( -5.000000000000000888, -1.924500897298784041, -3.818275046351167212 ) ) ;
#7396=ADVANCED_FACE ( 'NONE', ( #13373 ), #24831, .F. ) ;
#7431=DIRECTION ( 'NONE',  ( -0.000000000000000000, -0.000000000000000000, 1.000000000000000000 ) ) ;
#7453=CARTESIAN_POINT ( 'NONE',  ( -1.582370436567960503, -4.859920694386081763, -3.719399823475761480 ) ) ;
#7461=CARTESIAN_POINT ( 'NONE',  ( 0.7030283904599238243, 5.367609061416947824, -4.096693167835341320 ) ) ;
#7517=AXIS2_PLACEMENT_3D ( 'NONE', #24232, #12981, #15627 ) ;
#7633=CARTESIAN_POINT ( 'NONE',  ( -5.184911785340869272, 2.993510214990760865, -4.330720594357042152 ) ) ;
#7646=CARTESIAN_POINT ( 'NONE',  ( 4.999999999999999112, 0.2466074518009281902, -1.346217697502835001E-15 ) ) ;
#7689=ORIENTED_EDGE ( 'NONE', *, *, #23385, .F. ) ;
#7700=CARTESIAN_POINT ( 'NONE',  ( 2.500000000000021760, -4.330127018922177662, 0.000000000000000000 ) ) ;
#7718=B_SPLINE_CURVE_WITH_KNOTS ( 'NONE', 3,
 ( #1285, #6907, #10460, #24722, #29777, #18351, #4292, #32789 ),
 .UNSPECIFIED., .F., .F.,
 ( 4, 2, 2, 4 ),
 ( 2.451332856832783740E-07, 0.001475502392055661870, 0.002213131021440650163, 0.002950759650825637587 ),
 .UNSPECIFIED. ) ;
#7751=B_SPLINE_CURVE_WITH_KNOTS ( 'NONE', 3,
 ( #1375, #35354, #26693, #3816, #35154, #12794 ),
 .UNSPECIFIED., .F., .F.,
 ( 4, 2, 4 ),
 ( 0.000000000000000000, 0.0002514304509865740098, 0.0005028609019731480195 ),
 .UNSPECIFIED. ) ;
#7765=CARTESIAN_POINT ( 'NONE',  ( -5.253368672218637236, 3.033033817057754877, -4.359491423763649287 ) ) ;
#7785=EDGE_CURVE ( 'NONE', #28919, #4855, #3617, .T. ) ;
#7818=EDGE_CURVE ( 'NONE', #28919, #24399, #1523, .T. ) ;
#7844=CARTESIAN_POINT ( 'NONE',  ( 0.2117491801717968081, -5.895756138069173424, -4.027903350935069682 ) ) ;
#7851=ORIENTED_EDGE ( 'NONE', *, *, #5041, .T. ) ;
#7871=ADVANCED_FACE ( 'NONE', ( #15421 ), #19770, .T. ) ;
#7903=CARTESIAN_POINT ( 'NONE',  ( 5.244936596612841839, -2.071425061673250578, -4.180295101352479392 ) ) ;
#7906=CARTESIAN_POINT ( 'NONE',  ( 0.000000000000000000, 0.000000000000000000, 2.266666666666666607 ) ) ;
#8020=DIRECTION ( 'NONE',  ( -0.000000000000000000, -0.000000000000000000, 1.000000000000000000 ) ) ;
#8035=EDGE_CURVE ( 'NONE', #31719, #26481, #19211, .T. ) ;
#8059=DIRECTION ( 'NONE',  ( -0.9396926207859139790, 0.000000000000000000, -0.3420201433256533918 ) ) ;
#8068=EDGE_CURVE ( 'NONE', #18257, #19938, #4430, .T. ) ;
#8081=CARTESIAN_POINT ( 'NONE',  ( 4.166666666666666963, -3.367876570272838155, -3.818275046351167212 ) ) ;
#8160=VERTEX_POINT ( 'NONE', #16 ) ;
#8176=CARTESIAN_POINT ( 'NONE',  ( 4.999999999999999112, -2.886751345948144198, -3.984345921091770659 ) ) ;
#8182=CARTESIAN_POINT ( 'NONE',  ( -3.866666666667000651, 5.429267476220137302E-16, 3.400000000000000355 ) ) ;
#8193=PRODUCT_DEFINITION_FORMATION_WITH_SPECIFIED_SOURCE ( 'ANY', '', #34021, .NOT_KNOWN. ) ;
#8206=ORIENTED_EDGE ( 'NONE', *, *, #18021, .F. ) ;
#8279=CARTESIAN_POINT ( 'NONE',  ( 6.532899837730827386, 0.000000000000000000, -5.700000000000001066 ) ) ;
#8281=CARTESIAN_POINT ( 'NONE',  ( 5.253679167943698936, -3.068492024352256209, -4.366070081385298174 ) ) ;
#8295=ORIENTED_EDGE ( 'NONE', *, *, #9266, .T. ) ;
#8308=CARTESIAN_POINT ( 'NONE',  ( 0.000000000000000000, 0.000000000000000000, -5.674599999999998090 ) ) ;
#8329=CYLINDRICAL_SURFACE ( 'NONE', #28843, 2.500000000000000444 ) ;
#8337=CARTESIAN_POINT ( 'NONE',  ( -5.000000000000000888, -0.4954705650270051498, -2.700341035846709481E-15 ) ) ;
#8363=EDGE_CURVE ( 'NONE', #2722, #3797, #3110, .T. ) ;
#8468=CARTESIAN_POINT ( 'NONE',  ( -5.284804376168104945, 3.015249596956793177, -4.366192694417977194 ) ) ;
#8484=DIRECTION ( 'NONE',  ( -0.5000000000000014433, -0.8660254037844378194, 0.000000000000000000 ) ) ;
#8554=CARTESIAN_POINT ( 'NONE',  ( 4.999999999999997335, -0.9835753746177055001, -0.05800540215398956867 ) ) ;
#8569=DIRECTION ( 'NONE',  ( -0.000000000000000000, -0.000000000000000000, 1.000000000000000000 ) ) ;
#8572=CARTESIAN_POINT ( 'NONE',  ( 3.750000000000001776, 0.000000000000000000, 2.266666666666999674 ) ) ;
#8596=DIRECTION ( 'NONE',  ( 0.7071067811865486830, 0.000000000000000000, 0.7071067811865464625 ) ) ;
#8605=ORIENTED_EDGE ( 'NONE', *, *, #28294, .T. ) ;
#8625=CARTESIAN_POINT ( 'NONE',  ( 4.999999999999999112, -3.130590339601100780, -4.027780737902369346 ) ) ;
#8640=CARTESIAN_POINT ( 'NONE',  ( -5.029394918168152984, -2.903722509865350965, -4.151004066889661281 ) ) ;
#8663=CARTESIAN_POINT ( 'NONE',  ( 3.352586340487470729, 3.837886065734355423, -0.05822226285683193558 ) ) ;
#8664=ADVANCED_FACE ( 'NONE', ( #20957 ), #29671, .T. ) ;
#8669=FACE_OUTER_BOUND ( 'NONE', #27270, .T. ) ;
#8671=CARTESIAN_POINT ( 'NONE',  ( 5.236872748402764621, 8.442024233997350580E-14, -4.057689166958447835 ) ) ;
#8676=ADVANCED_FACE ( 'NONE', ( #29388 ), #26070, .T. ) ;
#8746=TOROIDAL_SURFACE ( 'NONE', #18231, 3.866666666667000651, 1.133333333332999793 ) ;
#8766=AXIS2_PLACEMENT_3D ( 'NONE', #28545, #19757, #5330 ) ;
#8805=VERTEX_POINT ( 'NONE', #22076 ) ;
#8809=EDGE_LOOP ( 'NONE', ( #23642, #23929, #30346, #28485 ) ) ;
#8896=CARTESIAN_POINT ( 'NONE',  ( 0.000000000000000000, 0.000000000000000000, 0.000000000000000000 ) ) ;
#8915=CARTESIAN_POINT ( 'NONE',  ( -2.500000000000000888, 4.330127018922190985, -3.620524600599875686 ) ) ;
#8920=DIRECTION ( 'NONE',  ( -0.000000000000000000, -0.000000000000000000, 1.000000000000000000 ) ) ;
#8946=DIRECTION ( 'NONE',  ( -0.000000000000000000, -0.000000000000000000, 1.000000000000000000 ) ) ;
#9010=CARTESIAN_POINT ( 'NONE',  ( -3.057313426867661832, -4.281874658697595315, -4.057628883416056098 ) ) ;
#9014=CARTESIAN_POINT ( 'NONE',  ( 0.000000000000000000, 0.000000000000000000, -25.03750572909317285 ) ) ;
#9025=CARTESIAN_POINT ( 'NONE',  ( -5.000000000000000888, 0.4965892259340443649, -0.01450341304856691757 ) ) ;
#9074=ORIENTED_EDGE ( 'NONE', *, *, #23385, .T. ) ;
#9110=EDGE_CURVE ( 'NONE', #32261, #24840, #9336, .T. ) ;
#9184=LINE ( 'NONE', #9378, #18850 ) ;
#9207=CARTESIAN_POINT ( 'NONE',  ( -6.069707180676227632E-15, 5.773502691896268857, -5.700000000000000178 ) ) ;
#9218=COLOUR_RGB ( '', 0.09019608, 0.27058824, 0.51372549) ;
#9240=CARTESIAN_POINT ( 'NONE',  ( 6.532899837730827386, 0.000000000000000000, -5.132899837730832360 ) ) ;
#9266=EDGE_CURVE ( 'NONE', #22867, #16872, #13230, .T. ) ;
#9280=CARTESIAN_POINT ( 'NONE',  ( 4.654160418576254177E-15, -6.066067634115602125, -4.359491423763670603 ) ) ;
#9322=AXIS2_PLACEMENT_3D ( 'NONE', #1727, #10339, #2636 ) ;
#9336=CIRCLE ( 'NONE', #19526, 3.000000000000000888 ) ;
#9378=CARTESIAN_POINT ( 'NONE',  ( -3.750000000000001776, 4.592425496802576930E-16, 13.31572692736085095 ) ) ;
#9386=CARTESIAN_POINT ( 'NONE',  ( -5.000000000000000000, 0.9888715124523126399, -0.07061148569344741222 ) ) ;
#9413=CARTESIAN_POINT ( 'NONE',  ( 4.999999999999999112, 2.886751345948125991, -3.984345921091767551 ) ) ;
#9431=ORIENTED_EDGE ( 'NONE', *, *, #855, .T. ) ;
#9515=LINE ( 'NONE', #1620, #15988 ) ;
#9586=CARTESIAN_POINT ( 'NONE',  ( -5.000000000000000000, 0.2466074518009242766, -2.689117849295589213E-15 ) ) ;
#9647=DIRECTION ( 'NONE',  ( 1.000000000000000000, 0.000000000000000000, 0.000000000000000000 ) ) ;
#9703=CARTESIAN_POINT ( 'NONE',  ( 0.000000000000000000, 0.000000000000000000, 0.000000000000000000 ) ) ;
#9724=CARTESIAN_POINT ( 'NONE',  ( -0.8333333333333292625, -5.292377467571617977, -3.818275046351179647 ) ) ;
#9834=ORIENTED_EDGE ( 'NONE', *, *, #13336, .T. ) ;
#9835=EDGE_CURVE ( 'NONE', #21285, #36512, #22351, .T. ) ;
#9864=DIRECTION ( 'NONE',  ( -0.000000000000000000, -0.000000000000000000, -1.000000000000000000 ) ) ;
#9870=VERTEX_POINT ( 'NONE', #32053 ) ;
#9927=CARTESIAN_POINT ( 'NONE',  ( 0.8082922630888169646, 5.306834936218043808, -0.2701150775513979641 ) ) ;
#10084=DIRECTION ( 'NONE',  ( 0.000000000000000000, 0.000000000000000000, 1.000000000000000000 ) ) ;
#10102=CIRCLE ( 'NONE', #5901, 2.500000000000000444 ) ;
#10129=DIRECTION ( 'NONE',  ( 0.5000000000000014433, 0.8660254037844378194, -0.000000000000000000 ) ) ;
#10132=CARTESIAN_POINT ( 'NONE',  ( -2.500000000000022204, 4.330127018922177662, 0.000000000000000000 ) ) ;
#10157=EDGE_CURVE ( 'NONE', #18000, #34714, #25493, .T. ) ;
#10168=AXIS2_PLACEMENT_3D ( 'NONE', #20945, #17949, #12283 ) ;
#10232=ORIENTED_EDGE ( 'NONE', *, *, #13222, .F. ) ;
#10339=DIRECTION ( 'NONE',  ( -0.000000000000000000, -0.000000000000000000, 1.000000000000000000 ) ) ;
#10355=CARTESIAN_POINT ( 'NONE',  ( -5.854691731421723944E-14, -5.773502691896269745, -0.5999999999999998668 ) ) ;
#10407=CARTESIAN_POINT ( 'NONE',  ( 0.000000000000000000, 0.000000000000000000, 0.000000000000000000 ) ) ;
#10428=B_SPLINE_CURVE_WITH_KNOTS ( 'NONE', 3,
 ( #10858, #31449, #5791, #36911, #22466, #17229 ),
 .UNSPECIFIED., .F., .F.,
 ( 4, 2, 4 ),
 ( 0.002950759650825688762, 0.004429055062152286240, 0.005907350473478884152 ),
 .UNSPECIFIED. ) ;
#10441=CONICAL_SURFACE ( 'NONE', #31385, 4.999999999999997335, 0.9110539511682894664 ) ;
#10455=CARTESIAN_POINT ( 'NONE',  ( 3.417629563432034612, 3.800333343458349944, -3.719399823475519895 ) ) ;
#10458=PRESENTATION_STYLE_ASSIGNMENT (( #24721 ) ) ;
#10460=CARTESIAN_POINT ( 'NONE',  ( -4.191707736911189031, 3.353419101626330612, -0.2701150775513885272 ) ) ;
#10494=ORIENTED_EDGE ( 'NONE', *, *, #31407, .F. ) ;
#10563=DIRECTION ( 'NONE',  ( 0.000000000000000000, 0.000000000000000000, -1.000000000000000000 ) ) ;
#10590=CARTESIAN_POINT ( 'NONE',  ( -5.204170427930421283E-15, 5.773502691896269745, -0.5999999999999998668 ) ) ;
#10606=CARTESIAN_POINT ( 'NONE',  ( 4.817220356105918810, -3.279784343982818040, -4.266919140436436386 ) ) ;
#10636=CARTESIAN_POINT ( 'NONE',  ( 5.000000000000007994, -2.886751345948139758, -0.5999999999999998668 ) ) ;
#10644=ORIENTED_EDGE ( 'NONE', *, *, #11713, .F. ) ;
#10645=CARTESIAN_POINT ( 'NONE',  ( 5.000000000000000000, 2.424500739214353384, -0.4207179063848189293 ) ) ;
#10663=ADVANCED_FACE ( 'NONE', ( #22098 ), #31051, .F. ) ;
#10676=DIRECTION ( 'NONE',  ( -1.000000000000000000, 1.224646799147350989E-16, 0.000000000000000000 ) ) ;
#10719=FACE_OUTER_BOUND ( 'NONE', #24229, .T. ) ;
#10768=CARTESIAN_POINT ( 'NONE',  ( 5.236872748402765509, -0.5081686017868810579, -4.057689166958444282 ) ) ;
#10854=ORIENTED_EDGE ( 'NONE', *, *, #5041, .F. ) ;
#10858=CARTESIAN_POINT ( 'NONE',  ( -2.500000000000006217, -4.330127018922186544, 0.000000000000000000 ) ) ;
#10892=CARTESIAN_POINT ( 'NONE',  ( -3.050000000000000711, 3.735172737399428132E-16, 2.266666666666999674 ) ) ;
#10897=CARTESIAN_POINT ( 'NONE',  ( 0.000000000000000000, 0.000000000000000000, -5.700000000000001066 ) ) ;
#10903=CARTESIAN_POINT ( 'NONE',  ( -4.400655246573244916, 3.515428273944189552, -4.176900509772079495 ) ) ;
#10905=CARTESIAN_POINT ( 'NONE',  ( 3.514986608498837484, -4.017641317389694322, -4.057689166958486915 ) ) ;
#10906=CARTESIAN_POINT ( 'NONE',  ( -2.285412292771023424, -4.454019289455668940, -2.909304063934346637E-14 ) ) ;
#11017=CIRCLE ( 'NONE', #26009, 3.750000000000001776 ) ;
#11027=CARTESIAN_POINT ( 'NONE',  ( 2.285412292771005660, 4.454019289455640518, -3.350862339338012141E-15 ) ) ;
#11032=CARTESIAN_POINT ( 'NONE',  ( 6.726859516510129922, 8.238026975208042369E-16, -4.599999999999999645 ) ) ;
#11041=ORIENTED_EDGE ( 'NONE', *, *, #9266, .F. ) ;
#11058=EDGE_LOOP ( 'NONE', ( #27920, #16394, #27861, #37107 ) ) ;
#11061=AXIS2_PLACEMENT_3D ( 'NONE', #20540, #8946, #31963 ) ;
#11068=CARTESIAN_POINT ( 'NONE',  ( 4.999999999999999112, 3.083561376477503835, -4.289114130331824981 ) ) ;
#11080=CARTESIAN_POINT ( 'NONE',  ( 5.000000000000000000, 0.000000000000000000, 2.266666666666666607 ) ) ;
#11148=( GEOMETRIC_REPRESENTATION_CONTEXT ( 3 ) GLOBAL_UNCERTAINTY_ASSIGNED_CONTEXT ( ( #32826 ) ) GLOBAL_UNIT_ASSIGNED_CONTEXT ( ( #26416, #32005, #24550 ) ) REPRESENTATION_CONTEXT ( 'NONE', 'WORKASPACE' ) );
#11169=DIRECTION ( 'NONE',  ( 1.000000000000000000, 0.000000000000000000, 0.000000000000000000 ) ) ;
#11174=VERTEX_POINT ( 'NONE', #31877 ) ;
#11283=CARTESIAN_POINT ( 'NONE',  ( -5.122335214190873565, -2.957381614792632618, -4.281769937709105633 ) ) ;
#11323=CARTESIAN_POINT ( 'NONE',  ( -4.999999999999997335, 0.000000000000000000, 0.000000000000000000 ) ) ;
#11387=DIRECTION ( 'NONE',  ( 1.000000000000000000, 0.000000000000000000, 0.000000000000000000 ) ) ;
#11402=AXIS2_PLACEMENT_3D ( 'NONE', #7906, #33970, #19527 ) ;
#11453=CARTESIAN_POINT ( 'NONE',  ( -4.296971609540364945, 3.292644976426615688, -4.096693167835493199 ) ) ;
#11495=CARTESIAN_POINT ( 'NONE',  ( -3.750000000000001776, 4.592425496802576930E-16, 3.400000000000000355 ) ) ;
#11533=ORIENTED_EDGE ( 'NONE', *, *, #28190, .F. ) ;
#11534=ORIENTED_EDGE ( 'NONE', *, *, #20142, .T. ) ;
#11542=APPLICATION_CONTEXT ( 'automotive_design' ) ;
#11571=CARTESIAN_POINT ( 'NONE',  ( -5.253679200383968073, 3.068495724078392328, -4.366070770724005179 ) ) ;
#11607=FACE_OUTER_BOUND ( 'NONE', #15380, .T. ) ;
#11699=CARTESIAN_POINT ( 'NONE',  ( 4.999999999999999112, 2.886751345948125991, -5.700000000000000178 ) ) ;
#11713=EDGE_CURVE ( 'NONE', #36735, #22867, #25280, .T. ) ;
#11802=CARTESIAN_POINT ( 'NONE',  ( -1.738710530748195815, -5.045296470310012715, -4.085927688751848308 ) ) ;
#11874=ORIENTED_EDGE ( 'NONE', *, *, #24575, .F. ) ;
#11885=DIRECTION ( 'NONE',  ( -0.000000000000000000, -0.000000000000000000, 1.000000000000000000 ) ) ;
#11899=DIRECTION ( 'NONE',  ( -0.000000000000000000, -0.000000000000000000, 1.000000000000000000 ) ) ;
#11908=ORIENTED_EDGE ( 'NONE', *, *, #6139, .T. ) ;
#11913=CARTESIAN_POINT ( 'NONE',  ( 4.390739357591695365E-15, -5.773502691896304384, -4.069522543421433269 ) ) ;
#11915=DIRECTION ( 'NONE',  ( 0.000000000000000000, 0.000000000000000000, 1.000000000000000000 ) ) ;
#11929=ORIENTED_EDGE ( 'NONE', *, *, #20142, .F. ) ;
#11977=ORIENTED_EDGE ( 'NONE', *, *, #28294, .F. ) ;
#12010=DIRECTION ( 'NONE',  ( 0.000000000000000000, 0.000000000000000000, 1.000000000000000000 ) ) ;
#12025=ORIENTED_EDGE ( 'NONE', *, *, #18820, .T. ) ;
#12171=CIRCLE ( 'NONE', #33758, 3.866666666667000651 ) ;
#12178=EDGE_CURVE ( 'NONE', #11174, #21285, #20324, .T. ) ;
#12195=B_SPLINE_CURVE_WITH_KNOTS ( 'NONE', 3,
 ( #36411, #30399, #2276, #8081, #13510 ),
 .UNSPECIFIED., .F., .F.,
 ( 4, 1, 4 ),
 ( 5.023827903067772009E-20, 0.002886751345948134623, 0.005773502691896269245 ),
 .UNSPECIFIED. ) ;
#12249=CIRCLE ( 'NONE', #19481, 3.050000000000000711 ) ;
#12250=CARTESIAN_POINT ( 'NONE',  ( 0.000000000000000000, 0.000000000000000000, 0.000000000000000000 ) ) ;
#12283=DIRECTION ( 'NONE',  ( 1.000000000000000000, 0.000000000000000000, 0.000000000000000000 ) ) ;
#12314=CARTESIAN_POINT ( 'NONE',  ( -5.284804376168106721, -3.015249596956847356, -4.366192694417986964 ) ) ;
#12367=CARTESIAN_POINT ( 'NONE',  ( -5.000000000000000888, 1.953108124182649563, -0.2699991669428306595 ) ) ;
#12439=CARTESIAN_POINT ( 'NONE',  ( -5.000000000000000888, -1.045018621958868854, -3.717859243272141789 ) ) ;
#12490=CARTESIAN_POINT ( 'NONE',  ( -5.000000000000000888, 2.886751345948107783, -5.700000000000000178 ) ) ;
#12495=CARTESIAN_POINT ( 'NONE',  ( 4.390739357591696154E-15, -5.773502691896305272, -3.984345921091785758 ) ) ;
#12525=EDGE_CURVE ( 'NONE', #1000, #27610, #28779, .T. ) ;
#12628=CARTESIAN_POINT ( 'NONE',  ( -5.000000000000000888, -2.094350244328533339, -3.837520945129150540 ) ) ;
#12640=DIRECTION ( 'NONE',  ( -0.000000000000000000, -0.000000000000000000, 1.000000000000000000 ) ) ;
#12720=CARTESIAN_POINT ( 'NONE',  ( 0.4012132626380134348, 5.541862106709760205, -0.4203182062997347090 ) ) ;
#12761=FACE_OUTER_BOUND ( 'NONE', #13524, .T. ) ;
#12794=CARTESIAN_POINT ( 'NONE',  ( 5.253368672218635460, 3.033033817057773529, -4.359491423763652840 ) ) ;
#12821=EDGE_LOOP ( 'NONE', ( #34404, #7689 ) ) ;
#12827=B_SPLINE_CURVE_WITH_KNOTS ( 'NONE', 3,
 ( #14322, #27813, #2689, #37018, #8337, #11323 ),
 .UNSPECIFIED., .F., .F.,
 ( 4, 2, 4 ),
 ( 0.004308305454211683143, 0.005784651566377464055, 0.007260997678543244099 ),
 .UNSPECIFIED. ) ;
#12898=ORIENTED_EDGE ( 'NONE', *, *, #33113, .T. ) ;
#12910=DIRECTION ( 'NONE',  ( -0.000000000000000000, -0.000000000000000000, 1.000000000000000000 ) ) ;
#12981=DIRECTION ( 'NONE',  ( -0.000000000000000000, -0.000000000000000000, 1.000000000000000000 ) ) ;
#13083=CARTESIAN_POINT ( 'NONE',  ( -0.6806757771963263259, -5.380514348701145089, -3.838711833383647853 ) ) ;
#13096=FILL_AREA_STYLE ('',( #36155 ) ) ;
#13157=AXIS2_PLACEMENT_3D ( 'NONE', #25834, #8020, #28088 ) ;
#13204=DIRECTION ( 'NONE',  ( 1.000000000000000000, 0.000000000000000000, 0.000000000000000000 ) ) ;
#13211=VERTEX_POINT ( 'NONE', #22177 ) ;
#13222=EDGE_CURVE ( 'NONE', #16872, #8805, #27029, .T. ) ;
#13230=LINE ( 'NONE', #32926, #5153 ) ;
#13250=CARTESIAN_POINT ( 'NONE',  ( -5.000000000000006217, 2.886751345948105563, -4.069520038198739087 ) ) ;
#13336=EDGE_CURVE ( 'NONE', #19938, #36735, #22137, .T. ) ;
#13341=CARTESIAN_POINT ( 'NONE',  ( 5.211749180171788787, -2.764497899775276935, -4.027903350935054583 ) ) ;
#13342=CARTESIAN_POINT ( 'NONE',  ( -2.500000000000006217, -4.330127018922186544, 0.000000000000000000 ) ) ;
#13367=AXIS2_PLACEMENT_3D ( 'NONE', #3250, #29110, #31741 ) ;
#13373=FACE_OUTER_BOUND ( 'NONE', #13907, .T. ) ;
#13405=ORIENTED_EDGE ( 'NONE', *, *, #32263, .T. ) ;
#13416=LINE ( 'NONE', #18523, #20754 ) ;
#13431=CARTESIAN_POINT ( 'NONE',  ( 5.000000000000000888, 1.953108124182682648, -0.2699991669428374874 ) ) ;
#13438=DIRECTION ( 'NONE',  ( 1.000000000000000000, 0.000000000000000000, 0.000000000000000000 ) ) ;
#13510=CARTESIAN_POINT ( 'NONE',  ( 4.999999999999999112, -2.886751345948144198, -3.984345921091770659 ) ) ;
#13524=EDGE_LOOP ( 'NONE', ( #29670, #5346, #13869, #2565 ) ) ;
#13554=PLANE ( 'NONE',  #7299 ) ;
#13568=VECTOR ( 'NONE', #980, 1000.000000000000000 ) ;
#13599=CARTESIAN_POINT ( 'NONE',  ( 3.866666666667000651, 0.000000000000000000, 3.400000000000000355 ) ) ;
#13614=CARTESIAN_POINT ( 'NONE',  ( 5.185163620696820352, -2.993655612201285621, -4.330826434870608033 ) ) ;
#13627=EDGE_LOOP ( 'NONE', ( #31851, #16180, #31045, #1789, #25510 ) ) ;
#13636=DIRECTION ( 'NONE',  ( 1.000000000000000000, 0.000000000000000000, 0.000000000000000000 ) ) ;
#13713=CARTESIAN_POINT ( 'NONE',  ( 4.999999999999999112, 1.044517492640908651, -3.717833924169676507 ) ) ;
#13731=CARTESIAN_POINT ( 'NONE',  ( -0.4012132626380694456, -5.541862106709765534, -0.4203182062997422030 ) ) ;
#13737=ORIENTED_EDGE ( 'NONE', *, *, #2811, .F. ) ;
#13815=DIRECTION ( 'NONE',  ( -0.000000000000000000, -0.000000000000000000, 1.000000000000000000 ) ) ;
#13869=ORIENTED_EDGE ( 'NONE', *, *, #31354, .F. ) ;
#13907=EDGE_LOOP ( 'NONE', ( #20473, #10494, #32086, #20072, #17878 ) ) ;
#13929=CARTESIAN_POINT ( 'NONE',  ( -6.216324218022825094E-15, 6.066067634115565710, -4.359491423763658169 ) ) ;
#13961=ADVANCED_FACE ( 'NONE', ( #15146 ), #36313, .F. ) ;
#13972=CARTESIAN_POINT ( 'NONE',  ( -5.236872748402766398, -8.269757189038523917E-14, -4.057689166958448723 ) ) ;
#14077=CARTESIAN_POINT ( 'NONE',  ( 0.03111943836865378732, 6.084399642271171693, -4.366192694417985187 ) ) ;
#14090=ADVANCED_FACE ( 'NONE', ( #292 ), #25825, .T. ) ;
#14091=ORIENTED_EDGE ( 'NONE', *, *, #19934, .F. ) ;
#14119=CONICAL_SURFACE ( 'NONE', #18922, 6.726859516510129922, 1.221730476396047038 ) ;
#14170=CIRCLE ( 'NONE', #8766, 1.133333333332999793 ) ;
#14193=CARTESIAN_POINT ( 'NONE',  ( -3.000000000000000888, 0.000000000000000000, -5.674599999999998090 ) ) ;
#14237=ORIENTED_EDGE ( 'NONE', *, *, #19104, .F. ) ;
#14285=CARTESIAN_POINT ( 'NONE',  ( -5.000000000000000888, -2.886751345948162406, -3.984345921091775100 ) ) ;
#14307=CARTESIAN_POINT ( 'NONE',  ( 2.930059260563441015, 4.081832189068400396, -3.399990250278760378E-15 ) ) ;
#14322=CARTESIAN_POINT ( 'NONE',  ( -5.000000000000000888, -2.886751345948150860, -0.5999999999999998668 ) ) ;
#14367=ORIENTED_EDGE ( 'NONE', *, *, #7818, .F. ) ;
#14385=AXIS2_PLACEMENT_3D ( 'NONE', #34874, #20055, #20596 ) ;
#14406=AXIS2_PLACEMENT_3D ( 'NONE', #1944, #26905, #33074 ) ;
#14412=CARTESIAN_POINT ( 'NONE',  ( -5.000000000000000888, 3.130594094869389554, -4.027781427241076351 ) ) ;
#14467=CYLINDRICAL_SURFACE ( 'NONE', #2788, 5.000000000000000888 ) ;
#14496=CARTESIAN_POINT ( 'NONE',  ( -0.4318028594007664034, 5.811705888748974758, -4.266911319714222550 ) ) ;
#14594=EDGE_CURVE ( 'NONE', #23996, #16004, #1206, .T. ) ;
#14671=VERTEX_POINT ( 'NONE', #7700 ) ;
#14682=DIRECTION ( 'NONE',  ( 0.000000000000000000, 0.000000000000000000, -1.000000000000000000 ) ) ;
#14722=CARTESIAN_POINT ( 'NONE',  ( 2.176667689905595005, 4.790324513057870881, -4.057749648769098272 ) ) ;
#14728=CARTESIAN_POINT ( 'NONE',  ( 4.468131147118817364E-15, -5.914770570062455768, -4.281776566113625115 ) ) ;
#14746=CARTESIAN_POINT ( 'NONE',  ( 5.236872748402764621, 8.442024233997350580E-14, -4.057689166958447835 ) ) ;
#14750=DIRECTION ( 'NONE',  ( 0.000000000000000000, 0.000000000000000000, 1.000000000000000000 ) ) ;
#14802=VECTOR ( 'NONE', #8059, 1000.000000000000000 ) ;
#14827=PRODUCT_DEFINITION ( 'UNKNOWN', '', #8193, #22309 ) ;
#14858=CARTESIAN_POINT ( 'NONE',  ( 0.8333333333333268200, 5.292377467571581562, -3.818275046351166768 ) ) ;
#14877=CARTESIAN_POINT ( 'NONE',  ( 3.567687560464448904, -3.713697318477654274, -0.1121614189353552921 ) ) ;
#14927=CARTESIAN_POINT ( 'NONE',  ( 0.000000000000000000, 0.000000000000000000, 3.400000000000000355 ) ) ;
#15022=CARTESIAN_POINT ( 'NONE',  ( -5.000000000000000888, 1.231908430319606618, -0.1119772403577100062 ) ) ;
#15053=ORIENTED_EDGE ( 'NONE', *, *, #10157, .F. ) ;
#15096=CARTESIAN_POINT ( 'NONE',  ( 0.8665032349992052296, 5.555903485205155867, -4.190643565754943900 ) ) ;
#15143=DIRECTION ( 'NONE',  ( -0.000000000000000000, -0.000000000000000000, 1.000000000000000000 ) ) ;
#15146=FACE_OUTER_BOUND ( 'NONE', #36664, .T. ) ;
#15159=CARTESIAN_POINT ( 'NONE',  ( -5.000000000000000888, -2.886751345948162406, -3.984345921091775100 ) ) ;
#15191=DIRECTION ( 'NONE',  ( -0.000000000000000000, -0.000000000000000000, 1.000000000000000000 ) ) ;
#15206=EDGE_LOOP ( 'NONE', ( #1073, #2821, #1749, #23792, #4455, #8206 ) ) ;
#15303=FACE_OUTER_BOUND ( 'NONE', #22523, .T. ) ;
#15333=VERTEX_POINT ( 'NONE', #13599 ) ;
#15334=CARTESIAN_POINT ( 'NONE',  ( -3.417629563432035500, -3.800333343458386359, -3.719399823475301847 ) ) ;
#15353=ORIENTED_EDGE ( 'NONE', *, *, #32263, .F. ) ;
#15358=EDGE_CURVE ( 'NONE', #34185, #18257, #23243, .T. ) ;
#15368=CARTESIAN_POINT ( 'NONE',  ( 0.000000000000000000, 3.750000000000001776, 3.400000000000000355 ) ) ;
#15380=EDGE_LOOP ( 'NONE', ( #20706, #17889, #7851, #15053, #19636, #22313, #23795 ) ) ;
#15381=DIRECTION ( 'NONE',  ( -0.000000000000000000, -0.000000000000000000, 1.000000000000000000 ) ) ;
#15421=FACE_OUTER_BOUND ( 'NONE', #20049, .T. ) ;
#15505=DIRECTION ( 'NONE',  ( -1.000000000000000000, 0.000000000000000000, 0.000000000000000000 ) ) ;
#15565=DIRECTION ( 'NONE',  ( 0.000000000000000000, 0.000000000000000000, -1.000000000000000000 ) ) ;
#15583=DIRECTION ( 'NONE',  ( 0.000000000000000000, 0.000000000000000000, 1.000000000000000000 ) ) ;
#15598=EDGE_CURVE ( 'NONE', #13211, #33059, #17509, .T. ) ;
#15608=CARTESIAN_POINT ( 'NONE',  ( 4.999999999999999112, 2.886751345948153968, -0.5999999999999998668 ) ) ;
#15615=B_SPLINE_CURVE_WITH_KNOTS ( 'NONE', 3,
 ( #31345, #14307, #8663, #33807, #16761, #28181 ),
 .UNSPECIFIED., .F., .F.,
 ( 4, 2, 4 ),
 ( 0.002950759650825675751, 0.004429055062152274097, 0.005907350473478872009 ),
 .UNSPECIFIED. ) ;
#15627=DIRECTION ( 'NONE',  ( 1.000000000000000000, 0.000000000000000000, 0.000000000000000000 ) ) ;
#15684=AXIS2_PLACEMENT_3D ( 'NONE', #21381, #15191, #579 ) ;
#15718=ORIENTED_EDGE ( 'NONE', *, *, #36489, .F. ) ;
#15802=VERTEX_POINT ( 'NONE', #16006 ) ;
#15819=ORIENTED_EDGE ( 'NONE', *, *, #27927, .T. ) ;
#15880=AXIS2_PLACEMENT_3D ( 'NONE', #27490, #32738, #6861 ) ;
#15926=CIRCLE ( 'NONE', #35712, 6.726859516510129922 ) ;
#15928=PLANE ( 'NONE',  #19453 ) ;
#15985=CIRCLE ( 'NONE', #36940, 3.866666666667000651 ) ;
#15988=VECTOR ( 'NONE', #1430, 1000.000000000000000 ) ;
#16004=VERTEX_POINT ( 'NONE', #24380 ) ;
#16006=CARTESIAN_POINT ( 'NONE',  ( -5.253368672218637236, 3.033033817057754877, -4.359491423763649287 ) ) ;
#16009=ORIENTED_EDGE ( 'NONE', *, *, #6043, .F. ) ;
#16056=CARTESIAN_POINT ( 'NONE',  ( -5.000000000000000888, -2.886751345948162406, -5.700000000000000178 ) ) ;
#16169=CARTESIAN_POINT ( 'NONE',  ( -5.000000000000000888, -2.710505431213761085E-14, -3.620524600599874798 ) ) ;
#16180=ORIENTED_EDGE ( 'NONE', *, *, #36489, .T. ) ;
#16189=ORIENTED_EDGE ( 'NONE', *, *, #24575, .T. ) ;
#16230=ADVANCED_FACE ( 'NONE', ( #17234 ), #3026, .F. ) ;
#16233=VERTEX_POINT ( 'NONE', #20501 ) ;
#16286=SURFACE_SIDE_STYLE ('',( #4671 ) ) ;
#16312=EDGE_CURVE ( 'NONE', #36034, #4855, #10102, .T. ) ;
#16327=EDGE_CURVE ( 'NONE', #18000, #15802, #17404, .T. ) ;
#16394=ORIENTED_EDGE ( 'NONE', *, *, #27069, .F. ) ;
#16410=DIRECTION ( 'NONE',  ( -1.000000000000000000, 0.000000000000000000, 0.000000000000000000 ) ) ;
#16448=CARTESIAN_POINT ( 'NONE',  ( -1.721886139904448276, -5.052888355616937055, -4.057689166958561522 ) ) ;
#16454=CARTESIAN_POINT ( 'NONE',  ( 4.319324222803677671, 3.279739689143281289, -3.838711833383739780 ) ) ;
#16522=CARTESIAN_POINT ( 'NONE',  ( 4.999999999999999112, -1.088215558004119066, -3.720998139100774260 ) ) ;
#16541=CARTESIAN_POINT ( 'NONE',  ( 0.8441225671311781698, -5.568793373801108615, -4.176900509771829029 ) ) ;
#16625=CARTESIAN_POINT ( 'NONE',  ( 0.8144415599836856146, -5.303284638000501872, -0.2680587191991445906 ) ) ;
#16633=EDGE_CURVE ( 'NONE', #3797, #27610, #15615, .T. ) ;
#16651=CARTESIAN_POINT ( 'NONE',  ( -0.2117491801717998334, 5.895756138069137009, -4.027903350935056359 ) ) ;
#16706=DIRECTION ( 'NONE',  ( 0.000000000000000000, 0.000000000000000000, -1.000000000000000000 ) ) ;
#16722=CARTESIAN_POINT ( 'NONE',  ( 5.236773920621756062, 1.020523963592002925, -4.056123266998443277 ) ) ;
#16733=ORIENTED_EDGE ( 'NONE', *, *, #2941, .F. ) ;
#16737=CARTESIAN_POINT ( 'NONE',  ( 0.2117491801717859834, 5.895756138069137009, -4.027903350935056359 ) ) ;
#16761=CARTESIAN_POINT ( 'NONE',  ( 4.597743007729422793, 3.118994528718954662, -0.4198507760575557746 ) ) ;
#16784=VECTOR ( 'NONE', #3101, 1000.000000000000000 ) ;
#16815=CARTESIAN_POINT ( 'NONE',  ( -5.000000000000000888, 6.123233995736767268E-16, 13.31572692736085095 ) ) ;
#16816=CARTESIAN_POINT ( 'NONE',  ( 5.029396762153802491, -2.903723574490945314, -4.151008977024209123 ) ) ;
#16820=CARTESIAN_POINT ( 'NONE',  ( 2.500000000000021760, -4.330127018922177662, 0.000000000000000000 ) ) ;
#16825=CARTESIAN_POINT ( 'NONE',  ( 4.999999999999999112, -1.947799557644004809, -0.2684016432552360221 ) ) ;
#16848=CARTESIAN_POINT ( 'NONE',  ( 3.000000000000000888, 3.673940397442060854E-16, -5.674599999999998090 ) ) ;
#16851=ORIENTED_EDGE ( 'NONE', *, *, #34447, .F. ) ;
#16862=ORIENTED_EDGE ( 'NONE', *, *, #26001, .T. ) ;
#16863=ORIENTED_EDGE ( 'NONE', *, *, #12525, .F. ) ;
#16872=VERTEX_POINT ( 'NONE', #30544 ) ;
#16885=VERTEX_POINT ( 'NONE', #16848 ) ;
#16916=PLANE ( 'NONE',  #17005 ) ;
#16968=EDGE_CURVE ( 'NONE', #28919, #23645, #35093, .T. ) ;
#17005=AXIS2_PLACEMENT_3D ( 'NONE', #16056, #8484, #19911 ) ;
#17060=EDGE_LOOP ( 'NONE', ( #35073, #30608 ) ) ;
#17082=CARTESIAN_POINT ( 'NONE',  ( -0.8441225671312687640, 5.568793373802039426, -4.176900509772169201 ) ) ;
#17099=FACE_OUTER_BOUND ( 'NONE', #26646, .T. ) ;
#17124=CARTESIAN_POINT ( 'NONE',  ( 4.999999999999999112, -1.924500897298765612, -3.818275046351163660 ) ) ;
#17126=DIRECTION ( 'NONE',  ( 1.000000000000000000, 0.000000000000000000, 0.000000000000000000 ) ) ;
#17127=VECTOR ( 'NONE', #36414, 1000.000000000000000 ) ;
#17138=CARTESIAN_POINT ( 'NONE',  ( 0.000000000000000000, 0.000000000000000000, 0.000000000000000000 ) ) ;
#17142=CARTESIAN_POINT ( 'NONE',  ( 0.000000000000000000, 0.000000000000000000, -5.674599999999998090 ) ) ;
#17155=EDGE_CURVE ( 'NONE', #8160, #31719, #9515, .T. ) ;
#17156=ORIENTED_EDGE ( 'NONE', *, *, #16312, .F. ) ;
#17229=CARTESIAN_POINT ( 'NONE',  ( -5.000000000000000888, -2.886751345948150860, -0.5999999999999998668 ) ) ;
#17234=FACE_OUTER_BOUND ( 'NONE', #24256, .T. ) ;
#17323=CARTESIAN_POINT ( 'NONE',  ( -3.060208875726633693, 4.280211771583961600, -4.057749648769094719 ) ) ;
#17339=DIRECTION ( 'NONE',  ( 0.000000000000000000, -1.000000000000000000, 0.000000000000000000 ) ) ;
#17348=CARTESIAN_POINT ( 'NONE',  ( 3.401922400366481192, 3.809401878282541176, -3.971474537231019397 ) ) ;
#17370=EDGE_CURVE ( 'NONE', #13211, #34185, #774, .T. ) ;
#17374=FILL_AREA_STYLE_COLOUR ( '', #9218 ) ;
#17404=B_SPLINE_CURVE_WITH_KNOTS ( 'NONE', 3,
 ( #26893, #22006, #33064, #30791, #24458, #7765 ),
 .UNSPECIFIED., .F., .F.,
 ( 4, 2, 4 ),
 ( 0.003058795990767257302, 0.004586520967003302265, 0.006114245943239346795 ),
 .UNSPECIFIED. ) ;
#17501=EDGE_LOOP ( 'NONE', ( #25775, #12898, #11874, #14367 ) ) ;
#17509=LINE ( 'NONE', #26333, #25020 ) ;
#17525=EDGE_CURVE ( 'NONE', #19938, #18000, #35212, .T. ) ;
#17526=CARTESIAN_POINT ( 'NONE',  ( 0.000000000000000000, 0.000000000000000000, 2.266666666666999674 ) ) ;
#17531=DIRECTION ( 'NONE',  ( 1.000000000000000000, 0.000000000000000000, 0.000000000000000000 ) ) ;
#17588=ORIENTED_EDGE ( 'NONE', *, *, #32975, .T. ) ;
#17610=CARTESIAN_POINT ( 'NONE',  ( -4.379424050594066919, -3.527728022193163504, -4.190801088233101268 ) ) ;
#17643=ORIENTED_EDGE ( 'NONE', *, *, #32436, .T. ) ;
#17674=DIRECTION ( 'NONE',  ( 1.000000000000000000, 0.000000000000000000, 0.000000000000000000 ) ) ;
#17697=CARTESIAN_POINT ( 'NONE',  ( -5.000000000000463629, -1.027024708428717181, -3.969883389773432025 ) ) ;
#17702=ORIENTED_EDGE ( 'NONE', *, *, #16633, .F. ) ;
#17706=CARTESIAN_POINT ( 'NONE',  ( -5.253368672218638125, -3.033033817057809500, -4.359491423763659945 ) ) ;
#17855=VERTEX_POINT ( 'NONE', #13929 ) ;
#17878=ORIENTED_EDGE ( 'NONE', *, *, #12525, .T. ) ;
#17889=ORIENTED_EDGE ( 'NONE', *, *, #33732, .T. ) ;
#17897=CARTESIAN_POINT ( 'NONE',  ( 0.000000000000000000, 0.000000000000000000, 2.266666666666999674 ) ) ;
#17937=ADVANCED_FACE ( 'NONE', ( #8669 ), #8329, .F. ) ;
#17949=DIRECTION ( 'NONE',  ( -0.000000000000000000, -0.000000000000000000, 1.000000000000000000 ) ) ;
#18000=VERTEX_POINT ( 'NONE', #6608 ) ;
#18007=EDGE_CURVE ( 'NONE', #1000, #30871, #26226, .T. ) ;
#18021=EDGE_CURVE ( 'NONE', #26481, #31719, #33668, .T. ) ;
#18038=ORIENTED_EDGE ( 'NONE', *, *, #9110, .T. ) ;
#18051=CARTESIAN_POINT ( 'NONE',  ( 2.714587707229039193, -4.206234748388752998, -2.383804823457777444E-14 ) ) ;
#18074=CARTESIAN_POINT ( 'NONE',  ( -5.000000000000000888, -3.131509683642110353, -4.027949516396631680 ) ) ;
#18112=EDGE_CURVE ( 'NONE', #18239, #36735, #2996, .T. ) ;
#18125=AXIS2_PLACEMENT_3D ( 'NONE', #27759, #2074, #19337 ) ;
#18132=DIRECTION ( 'NONE',  ( -1.000000000000000000, 0.000000000000000000, 0.000000000000000000 ) ) ;
#18133=ADVANCED_FACE ( 'NONE', ( #4346 ), #21603, .F. ) ;
#18162=AXIS2_PLACEMENT_3D ( 'NONE', #30129, #15143, #21700 ) ;
#18217=CARTESIAN_POINT ( 'NONE',  ( -6.216324218022825094E-15, 6.066067634115565710, -4.359491423763658169 ) ) ;
#18231=AXIS2_PLACEMENT_3D ( 'NONE', #32854, #21211, #24615 ) ;
#18239=VERTEX_POINT ( 'NONE', #2464 ) ;
#18257=VERTEX_POINT ( 'NONE', #6018 ) ;
#18279=VECTOR ( 'NONE', #11915, 1000.000000000000000 ) ;
#18351=CARTESIAN_POINT ( 'NONE',  ( -2.931639317407897849, 4.080919942823912017, -0.01465562841807576538 ) ) ;
#18393=DIRECTION ( 'NONE',  ( 1.000000000000000000, 0.000000000000000000, 0.000000000000000000 ) ) ;
#18424=DIRECTION ( 'NONE',  ( -0.8191520442889913545, 0.000000000000000000, -0.5735764363510468256 ) ) ;
#18505=EDGE_CURVE ( 'NONE', #3218, #34714, #22312, .T. ) ;
#18520=ADVANCED_FACE ( 'NONE', ( #2034 ), #34892, .F. ) ;
#18523=CARTESIAN_POINT ( 'NONE',  ( -5.000000000000000888, 2.886751345948107783, -5.700000000000000178 ) ) ;
#18553=SHAPE_REPRESENTATION_RELATIONSHIP ( 'NONE' , 'NONE' ,  #34443, #23302 ) ;
#18630=ORIENTED_EDGE ( 'NONE', *, *, #18505, .T. ) ;
#18664=ORIENTED_EDGE ( 'NONE', *, *, #18820, .F. ) ;
#18677=CARTESIAN_POINT ( 'NONE',  ( 2.179555516819077443, -4.788648424347467625, -4.057628883416056098 ) ) ;
#18704=CYLINDRICAL_SURFACE ( 'NONE', #19643, 2.500000000000000444 ) ;
#18709=CARTESIAN_POINT ( 'NONE',  ( 4.999999999999999112, 1.231908430319627934, -0.1119772403577117409 ) ) ;
#18712=CARTESIAN_POINT ( 'NONE',  ( -1.598077599632966805, -4.850852159561880761, -3.971474537231491908 ) ) ;
#18724=( NAMED_UNIT ( * ) SI_UNIT ( $, .STERADIAN. ) SOLID_ANGLE_UNIT ( ) );
#18780=CARTESIAN_POINT ( 'NONE',  ( -5.000000000000000888, 2.886751345948107783, -3.984345921091764886 ) ) ;
#18820=EDGE_CURVE ( 'NONE', #24840, #24399, #834, .T. ) ;
#18850=VECTOR ( 'NONE', #15381, 1000.000000000000000 ) ;
#18875=CARTESIAN_POINT ( 'NONE',  ( 5.122341571230610846, -2.957385285031219446, -4.281776566113608240 ) ) ;
#18879=CARTESIAN_POINT ( 'NONE',  ( -5.029394918168152984, 2.903722509865296342, -4.151004066889650623 ) ) ;
#18907=AXIS2_PLACEMENT_3D ( 'NONE', #9703, #7265, #18132 ) ;
#18922=AXIS2_PLACEMENT_3D ( 'NONE', #3574, #23818, #35064 ) ;
#18988=AXIS2_PLACEMENT_3D ( 'NONE', #9014, #28508, #573 ) ;
#19039=B_SPLINE_CURVE_WITH_KNOTS ( 'NONE', 3,
 ( #3443, #26483, #793, #14877, #626, #23674, #18051, #29471 ),
 .UNSPECIFIED., .F., .F.,
 ( 4, 2, 2, 4 ),
 ( 2.451332856729116966E-07, 0.001475502392055643005, 0.002213131021440628045, 0.002950759650825612868 ),
 .UNSPECIFIED. ) ;
#19099=CARTESIAN_POINT ( 'NONE',  ( 4.999999999999999112, 0.4965892259340526915, -0.01450341304856531295 ) ) ;
#19104=EDGE_CURVE ( 'NONE', #13211, #1000, #34249, .T. ) ;
#19106=ORIENTED_EDGE ( 'NONE', *, *, #18112, .F. ) ;
#19126=ORIENTED_EDGE ( 'NONE', *, *, #27061, .F. ) ;
#19139=CARTESIAN_POINT ( 'NONE',  ( -6.069707180676227632E-15, 5.773502691896269745, -4.069520038198747081 ) ) ;
#19149=AXIS2_PLACEMENT_3D ( 'NONE', #28178, #5324, #5119 ) ;
#19160=EDGE_LOOP ( 'NONE', ( #29758, #8605, #28269, #22702 ) ) ;
#19184=CARTESIAN_POINT ( 'NONE',  ( -1.598077599634237123, 4.850852159561235055, -3.971474537231017621 ) ) ;
#19198=ORIENTED_EDGE ( 'NONE', *, *, #25254, .F. ) ;
#19211=CIRCLE ( 'NONE', #11402, 5.000000000000000000 ) ;
#19265=DIRECTION ( 'NONE',  ( 1.000000000000000000, 0.000000000000000000, 0.000000000000000000 ) ) ;
#19337=DIRECTION ( 'NONE',  ( 1.000000000000000000, 0.000000000000000000, 0.000000000000000000 ) ) ;
#19342=AXIS2_PLACEMENT_3D ( 'NONE', #33161, #12910, #4128 ) ;
#19351=CARTESIAN_POINT ( 'NONE',  ( 4.296971609540542580, -3.292644976428869885, -4.096693167834889238 ) ) ;
#19453=AXIS2_PLACEMENT_3D ( 'NONE', #15368, #15565, #35824 ) ;
#19455=CARTESIAN_POINT ( 'NONE',  ( 1.598077599632994561, 4.850852159562153432, -3.971474537231019397 ) ) ;
#19477=CARTESIAN_POINT ( 'NONE',  ( -5.204170427930421283E-15, 5.773502691896269745, -0.5999999999999998668 ) ) ;
#19481=AXIS2_PLACEMENT_3D ( 'NONE', #17526, #11899, #28951 ) ;
#19491=CARTESIAN_POINT ( 'NONE',  ( 2.500000000000008438, 4.330127018922190096, -2.691222917490924395E-15 ) ) ;
#19526=AXIS2_PLACEMENT_3D ( 'NONE', #7280, #30329, #13438 ) ;
#19527=DIRECTION ( 'NONE',  ( 1.000000000000000000, 0.000000000000000000, 0.000000000000000000 ) ) ;
#19537=CARTESIAN_POINT ( 'NONE',  ( -5.170224855064532221, 2.788471980053834010, -4.289066185948678722 ) ) ;
#19617=CARTESIAN_POINT ( 'NONE',  ( 5.000000000000004441, -2.886751345948140646, -4.069522543421418170 ) ) ;
#19626=CARTESIAN_POINT ( 'NONE',  ( -5.122335214190873565, 2.957381614792576663, -4.281769937709094975 ) ) ;
#19636=ORIENTED_EDGE ( 'NONE', *, *, #16327, .T. ) ;
#19643=AXIS2_PLACEMENT_3D ( 'NONE', #3881, #10084, #32763 ) ;
#19659=AXIS2_PLACEMENT_3D ( 'NONE', #9207, #32067, #31716 ) ;
#19697=CARTESIAN_POINT ( 'NONE',  ( 0.000000000000000000, 0.000000000000000000, 0.000000000000000000 ) ) ;
#19712=CARTESIAN_POINT ( 'NONE',  ( 5.253687135845359180, 3.069400712291963096, -4.366239407765167613 ) ) ;
#19729=CARTESIAN_POINT ( 'NONE',  ( -5.253368672218638125, -3.033033817057809500, -4.359491423763659945 ) ) ;
#19733=DIRECTION ( 'NONE',  ( 0.000000000000000000, 0.000000000000000000, -1.000000000000000000 ) ) ;
#19757=DIRECTION ( 'NONE',  ( 0.000000000000000000, -1.000000000000000000, 0.000000000000000000 ) ) ;
#19770=CONICAL_SURFACE ( 'NONE', #22768, 4.999999999999997335, 0.9110539511682894664 ) ;
#19806=DIRECTION ( 'NONE',  ( -0.000000000000000000, -0.000000000000000000, 1.000000000000000000 ) ) ;
#19867=EDGE_CURVE ( 'NONE', #26674, #2722, #24315, .T. ) ;
#19881=FACE_OUTER_BOUND ( 'NONE', #18, .T. ) ;
#19891=DIRECTION ( 'NONE',  ( -0.000000000000000000, -0.000000000000000000, 1.000000000000000000 ) ) ;
#19907=CARTESIAN_POINT ( 'NONE',  ( 3.750000000000001776, 0.000000000000000000, 13.31572692736085095 ) ) ;
#19911=DIRECTION ( 'NONE',  ( 0.8660254037844378194, -0.5000000000000014433, 0.000000000000000000 ) ) ;
#19934=EDGE_CURVE ( 'NONE', #8805, #29715, #10428, .T. ) ;
#19938=VERTEX_POINT ( 'NONE', #30906 ) ;
#19965=CONICAL_SURFACE ( 'NONE', #13367, 4.999999999999997335, 0.9110539511682894664 ) ;
#20049=EDGE_LOOP ( 'NONE', ( #35688, #16733, #21056 ) ) ;
#20055=DIRECTION ( 'NONE',  ( 0.000000000000000000, 0.000000000000000000, -1.000000000000000000 ) ) ;
#20059=CARTESIAN_POINT ( 'NONE',  ( 4.999999999998231637, -2.092670831923694408, -4.100100627019599209 ) ) ;
#20067=ORIENTED_EDGE ( 'NONE', *, *, #16327, .F. ) ;
#20072=ORIENTED_EDGE ( 'NONE', *, *, #19104, .T. ) ;
#20109=DIRECTION ( 'NONE',  ( 1.000000000000000000, 0.000000000000000000, 0.000000000000000000 ) ) ;
#20120=CARTESIAN_POINT ( 'NONE',  ( -5.253368672218637236, 3.033033817057754877, -4.359491423763649287 ) ) ;
#20142=EDGE_CURVE ( 'NONE', #34714, #16004, #21762, .T. ) ;
#20168=CARTESIAN_POINT ( 'NONE',  ( -5.854691731421723944E-14, -5.773502691896269745, -0.5999999999999998668 ) ) ;
#20214=AXIS2_PLACEMENT_3D ( 'NONE', #4070, #9864, #21304 ) ;
#20284=ORIENTED_EDGE ( 'NONE', *, *, #5268, .F. ) ;
#20324=CIRCLE ( 'NONE', #10168, 3.750000000000001776 ) ;
#20347=VECTOR ( 'NONE', #18424, 999.9999999999998863 ) ;
#20351=CARTESIAN_POINT ( 'NONE',  ( -4.166666666666670515, 3.367876570272800407, -3.818275046351158775 ) ) ;
#20420=ADVANCED_FACE ( 'NONE', ( #17099 ), #16916, .T. ) ;
#20467=DIRECTION ( 'NONE',  ( -0.000000000000000000, -0.000000000000000000, 1.000000000000000000 ) ) ;
#20473=ORIENTED_EDGE ( 'NONE', *, *, #32436, .F. ) ;
#20489=DIRECTION ( 'NONE',  ( 0.000000000000000000, 0.000000000000000000, -1.000000000000000000 ) ) ;
#20501=CARTESIAN_POINT ( 'NONE',  ( -5.000000000000000888, 2.886751345948107783, -0.5999999999999836575 ) ) ;
#20508=CARTESIAN_POINT ( 'NONE',  ( -5.244800587397359770, -2.026986389275642786, -4.190560292650622465 ) ) ;
#20519=EDGE_CURVE ( 'NONE', #34191, #8805, #35567, .T. ) ;
#20540=CARTESIAN_POINT ( 'NONE',  ( 0.000000000000000000, 0.000000000000000000, -5.324496230895142901 ) ) ;
#20541=SHAPE_DEFINITION_REPRESENTATION ( #488, #34443 ) ;
#20596=DIRECTION ( 'NONE',  ( -1.000000000000000000, 0.000000000000000000, 0.000000000000000000 ) ) ;
#20610=ORIENTED_EDGE ( 'NONE', *, *, #8068, .T. ) ;
#20617=B_SPLINE_CURVE_WITH_KNOTS ( 'NONE', 3,
 ( #16820, #2387, #28607, #16625, #31235, #20168 ),
 .UNSPECIFIED., .F., .F.,
 ( 4, 2, 4 ),
 ( 0.002950759650825612868, 0.004429055062152258485, 0.005907350473478904102 ),
 .UNSPECIFIED. ) ;
#20646=CARTESIAN_POINT ( 'NONE',  ( 4.166666666666665186, 3.367876570272815950, -3.818275046351160995 ) ) ;
#20706=ORIENTED_EDGE ( 'NONE', *, *, #28190, .T. ) ;
#20716=SURFACE_STYLE_USAGE ( .BOTH. , #23540 ) ;
#20754=VECTOR ( 'NONE', #36318, 1000.000000000000000 ) ;
#20774=TOROIDAL_SURFACE ( 'NONE', #4637, 6.532899837730827386, 0.5671001622691684840 ) ;
#20800=DIRECTION ( 'NONE',  ( 0.000000000000000000, 0.000000000000000000, 1.000000000000000000 ) ) ;
#20805=CARTESIAN_POINT ( 'NONE',  ( -5.000000000000000888, -2.886751345948162406, -5.700000000000000178 ) ) ;
#20897=ADVANCED_FACE ( 'NONE', ( #5270 ), #10441, .T. ) ;
#20918=CARTESIAN_POINT ( 'NONE',  ( 1.738710530748193150, 5.045296470309976300, -4.085927688751835873 ) ) ;
#20945=CARTESIAN_POINT ( 'NONE',  ( 0.000000000000000000, 0.000000000000000000, 2.266666666666999674 ) ) ;
#20957=FACE_OUTER_BOUND ( 'NONE', #30170, .T. ) ;
#20970=CARTESIAN_POINT ( 'NONE',  ( -4.296971609540129577, -3.292644976428437342, -4.096693167836007454 ) ) ;
#20988=ORIENTED_EDGE ( 'NONE', *, *, #27397, .F. ) ;
#21056=ORIENTED_EDGE ( 'NONE', *, *, #21119, .F. ) ;
#21084=CARTESIAN_POINT ( 'NONE',  ( -3.000000000000000888, 3.673940397442060854E-16, -25.03750572909317285 ) ) ;
#21088=CARTESIAN_POINT ( 'NONE',  ( 4.379424050594064255, 3.527728022193126645, -4.190801088233093274 ) ) ;
#21119=EDGE_CURVE ( 'NONE', #16233, #26674, #7718, .T. ) ;
#21157=CARTESIAN_POINT ( 'NONE',  ( -4.166666666666667851, -3.367876570272852366, -3.818275046351169877 ) ) ;
#21165=EDGE_LOOP ( 'NONE', ( #3900, #21272, #9074, #35390 ) ) ;
#21173=FACE_BOUND ( 'NONE', #12821, .T. ) ;
#21211=DIRECTION ( 'NONE',  ( -0.000000000000000000, -0.000000000000000000, 1.000000000000000000 ) ) ;
#21218=LINE ( 'NONE', #27210, #13568 ) ;
#21272=ORIENTED_EDGE ( 'NONE', *, *, #31911, .T. ) ;
#21274=CARTESIAN_POINT ( 'NONE',  ( -4.999999999999997335, 0.000000000000000000, 0.000000000000000000 ) ) ;
#21285=VERTEX_POINT ( 'NONE', #8572 ) ;
#21304=DIRECTION ( 'NONE',  ( 1.000000000000000000, 0.000000000000000000, 0.000000000000000000 ) ) ;
#21321=AXIS2_PLACEMENT_3D ( 'NONE', #4327, #15583, #1701 ) ;
#21329=ORIENTED_EDGE ( 'NONE', *, *, #18007, .F. ) ;
#21349=MECHANICAL_DESIGN_GEOMETRIC_PRESENTATION_REPRESENTATION('',(#21944),#4613);
#21358=EDGE_LOOP ( 'NONE', ( #34357, #27753, #30047, #11929 ) ) ;
#21381=CARTESIAN_POINT ( 'NONE',  ( 0.000000000000000000, 0.000000000000000000, -5.132899837730832360 ) ) ;
#21385=AXIS2_PLACEMENT_3D ( 'NONE', #8896, #30384, #36396 ) ;
#21414=CARTESIAN_POINT ( 'NONE',  ( 0.000000000000000000, 0.000000000000000000, 0.000000000000000000 ) ) ;
#21562=DIRECTION ( 'NONE',  ( -0.8660254037844378194, 0.5000000000000014433, 0.000000000000000000 ) ) ;
#21571=ADVANCED_FACE ( 'NONE', ( #15303 ), #29931, .T. ) ;
#21603=CYLINDRICAL_SURFACE ( 'NONE', #18125, 3.750000000000001776 ) ;
#21606=FACE_OUTER_BOUND ( 'NONE', #22678, .T. ) ;
#21700=DIRECTION ( 'NONE',  ( 1.000000000000000000, 0.000000000000000000, 0.000000000000000000 ) ) ;
#21752=AXIS2_PLACEMENT_3D ( 'NONE', #34768, #34581, #25582 ) ;
#21762=CIRCLE ( 'NONE', #31421, 6.726859516510129922 ) ;
#21774=DIRECTION ( 'NONE',  ( -1.000000000000000000, 0.000000000000000000, 0.000000000000000000 ) ) ;
#21783=CARTESIAN_POINT ( 'NONE',  ( 4.319324222803831326, -3.279739689143214232, -3.838711833381958538 ) ) ;
#21847=DIRECTION ( 'NONE',  ( 0.000000000000000000, 0.000000000000000000, -1.000000000000000000 ) ) ;
#21873=EDGE_LOOP ( 'NONE', ( #2030, #17156, #13405, #25964 ) ) ;
#21893=AXIS2_PLACEMENT_3D ( 'NONE', #3488, #8920, #17531 ) ;
#21898=CARTESIAN_POINT ( 'NONE',  ( 1.582370436567959393, 4.859920694386045348, -3.719399823475519895 ) ) ;
#21900=( LENGTH_UNIT ( ) NAMED_UNIT ( * ) SI_UNIT ( .MILLI., .METRE. ) );
#21944=STYLED_ITEM ( 'NONE', ( #10458 ), #23302 ) ;
#22006=CARTESIAN_POINT ( 'NONE',  ( -5.236872748402767286, 0.5081686017868760619, -4.057689166958444282 ) ) ;
#22048=CARTESIAN_POINT ( 'NONE',  ( 4.378301941662549268, -3.528365556573306527, -4.190643565754943900 ) ) ;
#22075=CARTESIAN_POINT ( 'NONE',  ( -5.000000000000000888, 2.886751345948107783, -3.984345921091764886 ) ) ;
#22076=CARTESIAN_POINT ( 'NONE',  ( -2.500000000000006217, -4.330127018922186544, 0.000000000000000000 ) ) ;
#22092=CARTESIAN_POINT ( 'NONE',  ( -0.7030283904595745481, -5.367609061417498495, -4.096693167834930982 ) ) ;
#22098=FACE_OUTER_BOUND ( 'NONE', #5515, .T. ) ;
#22137=B_SPLINE_CURVE_WITH_KNOTS ( 'NONE', 3,
 ( #19729, #28328, #11283, #8640, #22902, #14285 ),
 .UNSPECIFIED., .F., .F.,
 ( 4, 2, 4 ),
 ( -3.988673288088376993E-06, 0.0002483701411510744260, 0.0005007289555902372366 ),
 .UNSPECIFIED. ) ;
#22167=ADVANCED_FACE ( 'NONE', ( #27995, #27623 ), #13554, .F. ) ;
#22169=AXIS2_PLACEMENT_3D ( 'NONE', #9240, #17339, #20489 ) ;
#22177=CARTESIAN_POINT ( 'NONE',  ( 4.999999999999999112, -2.886751345948144198, -3.984345921091770659 ) ) ;
#22267=TOROIDAL_SURFACE ( 'NONE', #15684, 6.532899837730827386, 0.5671001622691684840 ) ;
#22272=CARTESIAN_POINT ( 'NONE',  ( 4.400655246573196955, 3.515428273944452453, -4.176900509772112358 ) ) ;
#22309=PRODUCT_DEFINITION_CONTEXT ( 'detailed design', #4893, 'design' ) ;
#22312=CIRCLE ( 'NONE', #6138, 0.5671001622691687061 ) ;
#22313=ORIENTED_EDGE ( 'NONE', *, *, #33172, .T. ) ;
#22343=CARTESIAN_POINT ( 'NONE',  ( 0.1702248550645280023, 5.871782057790544407, -4.289066185948687604 ) ) ;
#22351=LINE ( 'NONE', #19907, #2823 ) ;
#22385=ORIENTED_EDGE ( 'NONE', *, *, #36666, .F. ) ;
#22444=ORIENTED_EDGE ( 'NONE', *, *, #27927, .F. ) ;
#22466=CARTESIAN_POINT ( 'NONE',  ( -4.597743007729434339, -3.118994528718985748, -0.4198507760575760361 ) ) ;
#22523=EDGE_LOOP ( 'NONE', ( #29352, #1556, #26844, #33210, #11041 ) ) ;
#22549=CARTESIAN_POINT ( 'NONE',  ( -3.000000000000000888, 3.673940397442060854E-16, -5.700000000000000178 ) ) ;
#22626=CARTESIAN_POINT ( 'NONE',  ( 0.000000000000000000, 0.000000000000000000, 3.400000000000000355 ) ) ;
#22671=CARTESIAN_POINT ( 'NONE',  ( -0.4022569922705816481, 5.541259509125439742, -0.4198507760575647119 ) ) ;
#22678=EDGE_LOOP ( 'NONE', ( #18664, #11908, #29265, #34290 ) ) ;
#22690=AXIS2_PLACEMENT_3D ( 'NONE', #17897, #28938, #22963 ) ;
#22702=ORIENTED_EDGE ( 'NONE', *, *, #35574, .F. ) ;
#22768=AXIS2_PLACEMENT_3D ( 'NONE', #21414, #33033, #21774 ) ;
#22867=VERTEX_POINT ( 'NONE', #12495 ) ;
#22900=CARTESIAN_POINT ( 'NONE',  ( -0.7030283904599151645, 5.367609061416117378, -4.096693167836310323 ) ) ;
#22902=CARTESIAN_POINT ( 'NONE',  ( -5.000000000000000888, -2.886751345948162406, -4.069520038198750633 ) ) ;
#22908=DIRECTION ( 'NONE',  ( -1.000000000000000000, 0.000000000000000000, 0.000000000000000000 ) ) ;
#22963=DIRECTION ( 'NONE',  ( 1.000000000000000000, 0.000000000000000000, 0.000000000000000000 ) ) ;
#23002=CYLINDRICAL_SURFACE ( 'NONE', #23904, 3.750000000000001776 ) ;
#23008=EDGE_CURVE ( 'NONE', #34191, #26481, #5379, .T. ) ;
#23051=ORIENTED_EDGE ( 'NONE', *, *, #36666, .T. ) ;
#23080=DIRECTION ( 'NONE',  ( -0.000000000000000000, -0.000000000000000000, 1.000000000000000000 ) ) ;
#23243=B_SPLINE_CURVE_WITH_KNOTS ( 'NONE', 3,
 ( #24499, #10606, #22048, #36491, #1970, #18677, #24858, #27658, #4974, #4423 ),
 .UNSPECIFIED., .F., .F.,
 ( 4, 2, 2, 2, 4 ),
 ( 0.000000000000000000, 0.001528561485809837349, 0.003057122971619674699, 0.004585684457429512265, 0.006114245943239349397 ),
 .UNSPECIFIED. ) ;
#23302=ADVANCED_BREP_SHAPE_REPRESENTATION ( '', ( #31591, #21385 ), #11148 ) ;
#23385=EDGE_CURVE ( 'NONE', #33080, #36512, #1652, .T. ) ;
#23501=DIRECTION ( 'NONE',  ( -1.000000000000000000, 0.000000000000000000, 0.000000000000000000 ) ) ;
#23519=CARTESIAN_POINT ( 'NONE',  ( -5.236971957347722473, 1.063004708247950125, -4.059261105226032562 ) ) ;
#23534=DIRECTION ( 'NONE',  ( 0.000000000000000000, 0.000000000000000000, 1.000000000000000000 ) ) ;
#23536=ORIENTED_EDGE ( 'NONE', *, *, #36156, .T. ) ;
#23540=SURFACE_SIDE_STYLE ('',( #3291 ) ) ;
#23556=CARTESIAN_POINT ( 'NONE',  ( 5.244800587397357106, 2.026986389275619249, -4.190560292650617136 ) ) ;
#23612=DIRECTION ( 'NONE',  ( 1.000000000000000000, 0.000000000000000000, -0.000000000000000000 ) ) ;
#23642=ORIENTED_EDGE ( 'NONE', *, *, #31911, .F. ) ;
#23645=VERTEX_POINT ( 'NONE', #26467 ) ;
#23674=CARTESIAN_POINT ( 'NONE',  ( 2.931639317407913392, -4.080919942823937774, -0.01465562841809941313 ) ) ;
#23731=EDGE_LOOP ( 'NONE', ( #28230, #10232, #23856 ) ) ;
#23752=CARTESIAN_POINT ( 'NONE',  ( 5.238704763094642836, 1.015773027556920338, -4.085839086323460378 ) ) ;
#23792=ORIENTED_EDGE ( 'NONE', *, *, #36236, .T. ) ;
#23795=ORIENTED_EDGE ( 'NONE', *, *, #32688, .T. ) ;
#23801=CARTESIAN_POINT ( 'NONE',  ( 4.390739357591696154E-15, -5.773502691896305272, -3.984345921091785758 ) ) ;
#23808=ORIENTED_EDGE ( 'NONE', *, *, #8363, .F. ) ;
#23814=AXIS2_PLACEMENT_3D ( 'NONE', #36081, #1570, #13204 ) ;
#23818=DIRECTION ( 'NONE',  ( 0.000000000000000000, 0.000000000000000000, -1.000000000000000000 ) ) ;
#23836=CARTESIAN_POINT ( 'NONE',  ( -5.000000000000000000, 2.424500739214314304, -0.4207179063848073275 ) ) ;
#23856=ORIENTED_EDGE ( 'NONE', *, *, #36645, .F. ) ;
#23904=AXIS2_PLACEMENT_3D ( 'NONE', #31961, #8569, #11387 ) ;
#23907=CARTESIAN_POINT ( 'NONE',  ( 0.000000000000000000, 0.000000000000000000, 1.716666666667001406 ) ) ;
#23929=ORIENTED_EDGE ( 'NONE', *, *, #35360, .F. ) ;
#23956=AXIS2_PLACEMENT_3D ( 'NONE', #12490, #15505, #14750 ) ;
#23980=EDGE_CURVE ( 'NONE', #22867, #13211, #12195, .T. ) ;
#23996=VERTEX_POINT ( 'NONE', #8279 ) ;
#24033=ORIENTED_EDGE ( 'NONE', *, *, #12178, .T. ) ;
#24060=ORIENTED_EDGE ( 'NONE', *, *, #31354, .T. ) ;
#24086=CARTESIAN_POINT ( 'NONE',  ( -0.8333333333333384774, 5.292377467571578009, -3.818275046351164104 ) ) ;
#24229=EDGE_LOOP ( 'NONE', ( #29449, #20988, #11533, #20284, #14237 ) ) ;
#24232=CARTESIAN_POINT ( 'NONE',  ( 0.000000000000000000, 0.000000000000000000, 2.266666666667000563 ) ) ;
#24249=ADVANCED_FACE ( 'NONE', ( #737, #29240 ), #3569, .F. ) ;
#24256=EDGE_LOOP ( 'NONE', ( #9834, #19106, #28992, #20067, #143 ) ) ;
#24315=B_SPLINE_CURVE_WITH_KNOTS ( 'NONE', 3,
 ( #10132, #25675, #35186, #25472, #22671, #19477 ),
 .UNSPECIFIED., .F., .F.,
 ( 4, 2, 4 ),
 ( 0.002950759650825637587, 0.004429055062152260219, 0.005907350473478882417 ),
 .UNSPECIFIED. ) ;
#24318=ADVANCED_FACE ( 'NONE', ( #29177 ), #23002, .F. ) ;
#24380=CARTESIAN_POINT ( 'NONE',  ( 6.726859516510129033, 0.000000000000000000, -4.599999999999999645 ) ) ;
#24399=VERTEX_POINT ( 'NONE', #14193 ) ;
#24458=CARTESIAN_POINT ( 'NONE',  ( -5.248988766908547099, 2.532174945215621253, -4.266961984436636435 ) ) ;
#24480=EDGE_LOOP ( 'NONE', ( #34698, #6431, #35071, #888 ) ) ;
#24495=ORIENTED_EDGE ( 'NONE', *, *, #27739, .T. ) ;
#24496=CONICAL_SURFACE ( 'NONE', #22690, 3.050000000000000711, 0.7853981633974498333 ) ;
#24499=CARTESIAN_POINT ( 'NONE',  ( 5.253368672218635460, -3.033033817057790404, -4.359491423763655504 ) ) ;
#24508=ADVANCED_FACE ( 'NONE', ( #6259 ), #24496, .F. ) ;
#24511=ORIENTED_EDGE ( 'NONE', *, *, #32975, .F. ) ;
#24540=CARTESIAN_POINT ( 'NONE',  ( 0.03111943836866551752, -6.084399642271208997, -4.366192694417998510 ) ) ;
#24548=CARTESIAN_POINT ( 'NONE',  ( 1.721886139904373003, 5.052888355616772742, -4.057689166958494020 ) ) ;
#24550=( NAMED_UNIT ( * ) SI_UNIT ( $, .STERADIAN. ) SOLID_ANGLE_UNIT ( ) );
#24566=VECTOR ( 'NONE', #31543, 1000.000000000000000 ) ;
#24569=DIRECTION ( 'NONE',  ( 1.224646799147353207E-16, 1.000000000000000000, 0.000000000000000000 ) ) ;
#24575=EDGE_CURVE ( 'NONE', #24399, #16885, #34664, .T. ) ;
#24615=DIRECTION ( 'NONE',  ( 1.000000000000000000, 0.000000000000000000, 0.000000000000000000 ) ) ;
#24660=EDGE_CURVE ( 'NONE', #32261, #16885, #1374, .T. ) ;
#24700=ORIENTED_EDGE ( 'NONE', *, *, #30580, .F. ) ;
#24711=CARTESIAN_POINT ( 'NONE',  ( 0.000000000000000000, 0.000000000000000000, -5.674599999999998090 ) ) ;
#24721=SURFACE_STYLE_USAGE ( .BOTH. , #16286 ) ;
#24722=CARTESIAN_POINT ( 'NONE',  ( -3.567687560464436025, 3.713697318477624520, -0.1121614189353325186 ) ) ;
#24733=EDGE_CURVE ( 'NONE', #26481, #36697, #5969, .T. ) ;
#24799=CARTESIAN_POINT ( 'NONE',  ( 1.598077599633028090, -4.850852159562031751, -3.971474537231029611 ) ) ;
#24819=DIRECTION ( 'NONE',  ( -1.000000000000000000, 0.000000000000000000, -0.000000000000000000 ) ) ;
#24831=PLANE ( 'NONE',  #14406 ) ;
#24840=VERTEX_POINT ( 'NONE', #22549 ) ;
#24858=CARTESIAN_POINT ( 'NONE',  ( 1.738521435313294727, -5.045405839192998343, -4.085926550512748001 ) ) ;
#24886=CARTESIAN_POINT ( 'NONE',  ( 4.999999999999997335, 0.000000000000000000, 0.000000000000000000 ) ) ;
#24974=CARTESIAN_POINT ( 'NONE',  ( -4.999999999999999112, 1.924500897298729196, -3.818275046351159219 ) ) ;
#24977=LINE ( 'NONE', #10892, #17127 ) ;
#24991=CARTESIAN_POINT ( 'NONE',  ( 4.400655246572464208, -3.515428273943662862, -4.176900509771739323 ) ) ;
#25020=VECTOR ( 'NONE', #3262, 1000.000000000000000 ) ;
#25083=CARTESIAN_POINT ( 'NONE',  ( 4.999999999999999112, 2.886751345948125991, -3.984345921091767551 ) ) ;
#25170=CARTESIAN_POINT ( 'NONE',  ( 4.999999999999998224, 1.026530412860235053, -3.969857242416569232 ) ) ;
#25186=CARTESIAN_POINT ( 'NONE',  ( 1.582370436567792638, -4.859920694386177686, -3.719399823475529665 ) ) ;
#25187=CARTESIAN_POINT ( 'NONE',  ( -0.8082922630888651483, -5.306834936218053578, -0.2701150775514121749 ) ) ;
#25254=EDGE_CURVE ( 'NONE', #4855, #36034, #2386, .T. ) ;
#25280=B_SPLINE_CURVE_WITH_KNOTS ( 'NONE', 3,
 ( #15159, #21157, #26595, #9724, #23801 ),
 .UNSPECIFIED., .F., .F.,
 ( 4, 1, 4 ),
 ( 0.000000000000000000, 0.002886751345948134623, 0.005773502691896269245 ),
 .UNSPECIFIED. ) ;
#25322=ADVANCED_FACE ( 'NONE', ( #32376 ), #3314, .T. ) ;
#25327=CARTESIAN_POINT ( 'NONE',  ( -5.000000000000000000, 6.123233995736766282E-16, 2.266666666666666607 ) ) ;
#25331=B_SPLINE_CURVE_WITH_KNOTS ( 'NONE', 3,
 ( #33741, #33371, #36564, #4697, #19139, #2239 ),
 .UNSPECIFIED., .F., .F.,
 ( 4, 2, 4 ),
 ( -3.988673288092903537E-06, 0.0002483701411510707939, 0.0005007289555902344176 ),
 .UNSPECIFIED. ) ;
#25332=CARTESIAN_POINT ( 'NONE',  ( 4.999999999999999112, 3.131512667671952688, -4.027950064282237896 ) ) ;
#25345=CARTESIAN_POINT ( 'NONE',  ( -3.514986608498369414, 4.017641317390100220, -4.057689166958530436 ) ) ;
#25472=CARTESIAN_POINT ( 'NONE',  ( -0.8144415599836954955, 5.303284638000461015, -0.2680587191991145590 ) ) ;
#25493=LINE ( 'NONE', #33754, #14802 ) ;
#25510=ORIENTED_EDGE ( 'NONE', *, *, #855, .F. ) ;
#25571=CARTESIAN_POINT ( 'NONE',  ( 4.999999999999999112, -8.890457814381136359E-15, -3.620524600599876575 ) ) ;
#25582=DIRECTION ( 'NONE',  ( 1.000000000000000000, 0.000000000000000000, 0.000000000000000000 ) ) ;
#25595=B_SPLINE_CURVE_WITH_KNOTS ( 'NONE', 3,
 ( #3400, #9586, #9025, #9386, #15022, #12367, #23836, #31866 ),
 .UNSPECIFIED., .F., .F.,
 ( 4, 2, 2, 4 ),
 ( 0.007260997678543244099, 0.007995810154593281649, 0.008730622630643319199, 0.01020024758274339430 ),
 .UNSPECIFIED. ) ;
#25675=CARTESIAN_POINT ( 'NONE',  ( -2.069940739436584298, 4.578421848775973579, -1.448426339804853087E-16 ) ) ;
#25685=CARTESIAN_POINT ( 'NONE',  ( 3.050000000000000711, 0.000000000000000000, 2.266666666666999674 ) ) ;
#25702=EDGE_LOOP ( 'NONE', ( #31879, #24511, #14091 ) ) ;
#25714=CARTESIAN_POINT ( 'NONE',  ( 4.999999999999998224, -3.082650397928314856, -4.288940341510108389 ) ) ;
#25766=CARTESIAN_POINT ( 'NONE',  ( 5.238715782502660900, -1.018209582082221454, -4.086015505371661583 ) ) ;
#25771=DIRECTION ( 'NONE',  ( -0.000000000000000000, -0.000000000000000000, 1.000000000000000000 ) ) ;
#25775=ORIENTED_EDGE ( 'NONE', *, *, #16968, .T. ) ;
#25825=CYLINDRICAL_SURFACE ( 'NONE', #31701, 5.000000000000000888 ) ;
#25834=CARTESIAN_POINT ( 'NONE',  ( 0.000000000000000000, 0.000000000000000000, 1.716666666667001406 ) ) ;
#25837=ORIENTED_EDGE ( 'NONE', *, *, #8035, .F. ) ;
#25855=LINE ( 'NONE', #25685, #28435 ) ;
#25964=ORIENTED_EDGE ( 'NONE', *, *, #32671, .T. ) ;
#25984=DIRECTION ( 'NONE',  ( -0.000000000000000000, -0.000000000000000000, 1.000000000000000000 ) ) ;
#26001=EDGE_CURVE ( 'NONE', #31719, #15333, #14170, .T. ) ;
#26009=AXIS2_PLACEMENT_3D ( 'NONE', #14927, #25984, #669 ) ;
#26070=CONICAL_SURFACE ( 'NONE', #34483, 6.726859516510129922, 1.221730476396047038 ) ;
#26087=TOROIDAL_SURFACE ( 'NONE', #7517, 3.866666666667000651, 1.133333333332999793 ) ;
#26113=CARTESIAN_POINT ( 'NONE',  ( 5.000000000000007994, -2.886751345948139758, -0.5999999999999998668 ) ) ;
#26226=B_SPLINE_CURVE_WITH_KNOTS ( 'NONE', 3,
 ( #9413, #20646, #6222, #14858, #32076 ),
 .UNSPECIFIED., .F., .F.,
 ( 4, 1, 4 ),
 ( 0.000000000000000000, 0.002886751345948134623, 0.005773502691896269245 ),
 .UNSPECIFIED. ) ;
#26289=FACE_OUTER_BOUND ( 'NONE', #13627, .T. ) ;
#26309=CARTESIAN_POINT ( 'NONE',  ( -3.499999647538295289, 4.028415724610438176, -4.085927688751829656 ) ) ;
#26333=CARTESIAN_POINT ( 'NONE',  ( 4.999999999999999112, -2.886751345948144198, -5.700000000000000178 ) ) ;
#26398=DIRECTION ( 'NONE',  ( 0.000000000000000000, 0.000000000000000000, -1.000000000000000000 ) ) ;
#26416=( LENGTH_UNIT ( ) NAMED_UNIT ( * ) SI_UNIT ( .MILLI., .METRE. ) );
#26467=CARTESIAN_POINT ( 'NONE',  ( 2.500000000000000444, 0.000000000000000000, -5.324496230895142901 ) ) ;
#26481=VERTEX_POINT ( 'NONE', #25327 ) ;
#26483=CARTESIAN_POINT ( 'NONE',  ( 4.598786737361995947, -3.118391931134647077, -0.4203182062997404822 ) ) ;
#26507=CARTESIAN_POINT ( 'NONE',  ( 0.000000000000000000, 0.000000000000000000, -5.674599999999998090 ) ) ;
#26525=CARTESIAN_POINT ( 'NONE',  ( 3.500188911486798560, 4.028306647601576529, -4.085926550512734678 ) ) ;
#26580=CARTESIAN_POINT ( 'NONE',  ( -5.211749180171792339, -2.764497899775295586, -4.027903350935058135 ) ) ;
#26595=CARTESIAN_POINT ( 'NONE',  ( -2.499999999999996891, -4.330127018922233617, -3.620524600599889453 ) ) ;
#26609=ORIENTED_EDGE ( 'NONE', *, *, #11713, .T. ) ;
#26627=EDGE_LOOP ( 'NONE', ( #916, #428, #25837, #32989, #6310, #27582 ) ) ;
#26646=EDGE_LOOP ( 'NONE', ( #26609, #8295, #35894, #29950, #22444 ) ) ;
#26674=VERTEX_POINT ( 'NONE', #558 ) ;
#26693=CARTESIAN_POINT ( 'NONE',  ( 5.029396762153803380, 2.903723574490927994, -4.151008977024205571 ) ) ;
#26743=CARTESIAN_POINT ( 'NONE',  ( 5.253368672218635460, 3.033033817057773529, -4.359491423763652840 ) ) ;
#26844=ORIENTED_EDGE ( 'NONE', *, *, #34447, .T. ) ;
#26890=AXIS2_PLACEMENT_3D ( 'NONE', #26507, #11885, #34600 ) ;
#26893=CARTESIAN_POINT ( 'NONE',  ( -5.236872748402766398, -8.269757189038523917E-14, -4.057689166958448723 ) ) ;
#26905=DIRECTION ( 'NONE',  ( -1.000000000000000000, 0.000000000000000000, 0.000000000000000000 ) ) ;
#27004=FACE_OUTER_BOUND ( 'NONE', #21358, .T. ) ;
#27029=B_SPLINE_CURVE_WITH_KNOTS ( 'NONE', 3,
 ( #10355, #13731, #25187, #27776, #36612, #28165, #10906, #13342 ),
 .UNSPECIFIED., .F., .F.,
 ( 4, 2, 2, 4 ),
 ( 2.451332857604987150E-07, 0.001475502392055724754, 0.002213131021440706107, 0.002950759650825688762 ),
 .UNSPECIFIED. ) ;
#27030=CARTESIAN_POINT ( 'NONE',  ( -3.000000000000000888, 0.000000000000000000, -5.674599999999998090 ) ) ;
#27061=EDGE_CURVE ( 'NONE', #32911, #35959, #12249, .T. ) ;
#27069=EDGE_CURVE ( 'NONE', #30871, #18239, #28207, .T. ) ;
#27162=AXIS2_PLACEMENT_3D ( 'NONE', #6762, #12010, #29271 ) ;
#27210=CARTESIAN_POINT ( 'NONE',  ( 2.500000000000000444, 0.000000000000000000, -5.700000000000000178 ) ) ;
#27226=CIRCLE ( 'NONE', #11061, 2.500000000000000444 ) ;
#27270=EDGE_LOOP ( 'NONE', ( #6647, #27636, #32455, #28236 ) ) ;
#27329=CARTESIAN_POINT ( 'NONE',  ( -0.8441225671309252609, -5.568793373801227631, -4.176900509771872549 ) ) ;
#27397=EDGE_CURVE ( 'NONE', #9870, #34185, #895, .T. ) ;
#27408=CYLINDRICAL_SURFACE ( 'NONE', #9322, 3.000000000000000888 ) ;
#27475=CARTESIAN_POINT ( 'NONE',  ( 2.500000000000000444, 0.000000000000000000, 1.716666666667001406 ) ) ;
#27490=CARTESIAN_POINT ( 'NONE',  ( 4.390739357591696154E-15, -5.773502691896305272, -5.700000000000000178 ) ) ;
#27507=CARTESIAN_POINT ( 'NONE',  ( -5.253368672218637236, 3.033033817057754877, -4.359491423763649287 ) ) ;
#27582=ORIENTED_EDGE ( 'NONE', *, *, #2811, .T. ) ;
#27608=ORIENTED_EDGE ( 'NONE', *, *, #32688, .F. ) ;
#27610=VERTEX_POINT ( 'NONE', #15608 ) ;
#27623=FACE_OUTER_BOUND ( 'NONE', #33010, .T. ) ;
#27636=ORIENTED_EDGE ( 'NONE', *, *, #7785, .T. ) ;
#27658=CARTESIAN_POINT ( 'NONE',  ( 0.8653900595644530291, -5.556556492855614593, -4.190801088233106597 ) ) ;
#27677=ADVANCED_FACE ( 'NONE', ( #12761 ), #8746, .T. ) ;
#27724=ADVANCED_FACE ( 'NONE', ( #21606 ), #27408, .F. ) ;
#27739=EDGE_CURVE ( 'NONE', #4855, #32911, #24977, .T. ) ;
#27753=ORIENTED_EDGE ( 'NONE', *, *, #30580, .T. ) ;
#27759=CARTESIAN_POINT ( 'NONE',  ( 0.000000000000000000, 0.000000000000000000, 13.31572692736085095 ) ) ;
#27776=CARTESIAN_POINT ( 'NONE',  ( -1.432312439535614379, -4.946556719366762778, -0.1121614189353595248 ) ) ;
#27813=CARTESIAN_POINT ( 'NONE',  ( -5.000000000000000000, -2.426004080355352421, -0.4213009713786332044 ) ) ;
#27861=ORIENTED_EDGE ( 'NONE', *, *, #33845, .F. ) ;
#27904=ADVANCED_FACE ( 'NONE', ( #11607 ), #14119, .T. ) ;
#27920=ORIENTED_EDGE ( 'NONE', *, *, #998, .T. ) ;
#27927=EDGE_CURVE ( 'NONE', #36735, #29715, #3186, .T. ) ;
#27940=DIRECTION ( 'NONE',  ( -1.000000000000000000, 0.000000000000000000, 0.000000000000000000 ) ) ;
#27953=CARTESIAN_POINT ( 'NONE',  ( 4.999999999999999112, -1.069697119166215682, -3.973125653578879035 ) ) ;
#27961=ORIENTED_EDGE ( 'NONE', *, *, #18112, .T. ) ;
#27971=CARTESIAN_POINT ( 'NONE',  ( -0.03111943836865636165, -6.084399642271208997, -4.366192694417998510 ) ) ;
#27995=FACE_BOUND ( 'NONE', #34536, .T. ) ;
#28073=AXIS2_PLACEMENT_3D ( 'NONE', #17142, #14682, #23501 ) ;
#28088=DIRECTION ( 'NONE',  ( 1.000000000000000000, 0.000000000000000000, 0.000000000000000000 ) ) ;
#28104=CARTESIAN_POINT ( 'NONE',  ( 2.500000000000008438, 4.330127018922190096, -2.691222917490924395E-15 ) ) ;
#28115=ADVANCED_FACE ( 'NONE', ( #21173, #4132 ), #15928, .F. ) ;
#28147=CARTESIAN_POINT ( 'NONE',  ( 5.000000000000000000, 2.068880869914945020, -4.095521153410206949 ) ) ;
#28150=ADVANCED_FACE ( 'NONE', ( #32807 ), #4311, .T. ) ;
#28165=CARTESIAN_POINT ( 'NONE',  ( -2.068360682592148336, -4.579334095020483275, -0.01465562841810411250 ) ) ;
#28178=CARTESIAN_POINT ( 'NONE',  ( -3.866666666667000651, 4.735300956703508322E-16, 2.266666666667000563 ) ) ;
#28181=CARTESIAN_POINT ( 'NONE',  ( 4.999999999999999112, 2.886751345948153968, -0.5999999999999998668 ) ) ;
#28187=CARTESIAN_POINT ( 'NONE',  ( 0.000000000000000000, 0.000000000000000000, -5.700000000000000178 ) ) ;
#28190=EDGE_CURVE ( 'NONE', #35211, #9870, #5756, .T. ) ;
#28205=ORIENTED_EDGE ( 'NONE', *, *, #31407, .T. ) ;
#28207=B_SPLINE_CURVE_WITH_KNOTS ( 'NONE', 3,
 ( #6273, #24086, #8915, #20351, #6655 ),
 .UNSPECIFIED., .F., .F.,
 ( 4, 1, 4 ),
 ( 6.279784878834714258E-20, 0.002886751345948134623, 0.005773502691896268378 ),
 .UNSPECIFIED. ) ;
#28230=ORIENTED_EDGE ( 'NONE', *, *, #32760, .F. ) ;
#28236=ORIENTED_EDGE ( 'NONE', *, *, #33235, .F. ) ;
#28269=ORIENTED_EDGE ( 'NONE', *, *, #7818, .T. ) ;
#28285=CARTESIAN_POINT ( 'NONE',  ( 3.000000000000000888, 0.000000000000000000, -5.700000000000000178 ) ) ;
#28294=EDGE_CURVE ( 'NONE', #23645, #28919, #27226, .T. ) ;
#28318=EDGE_LOOP ( 'NONE', ( #19198, #24495, #30776, #15353 ) ) ;
#28328=CARTESIAN_POINT ( 'NONE',  ( -5.184911785340888812, -2.993510214990782625, -4.330720594357050146 ) ) ;
#28435=VECTOR ( 'NONE', #8596, 1000.000000000000000 ) ;
#28464=CIRCLE ( 'NONE', #21893, 3.050000000000000711 ) ;
#28485=ORIENTED_EDGE ( 'NONE', *, *, #31574, .T. ) ;
#28503=CARTESIAN_POINT ( 'NONE',  ( -2.176667689905596337, -4.790324513057907296, -4.057749648769110706 ) ) ;
#28508=DIRECTION ( 'NONE',  ( -0.000000000000000000, -0.000000000000000000, 1.000000000000000000 ) ) ;
#28545=CARTESIAN_POINT ( 'NONE',  ( 3.866666666667000651, 0.000000000000000000, 2.266666666667000563 ) ) ;
#28583=CARTESIAN_POINT ( 'NONE',  ( -0.1702248550645419911, 5.871782057790544407, -4.289066185948687604 ) ) ;
#28607=CARTESIAN_POINT ( 'NONE',  ( 1.647413659512552364, -4.822367972110057188, -0.05822226285685519476 ) ) ;
#28622=CARTESIAN_POINT ( 'NONE',  ( 0.000000000000000000, 0.000000000000000000, 13.31572692736085095 ) ) ;
#28641=CARTESIAN_POINT ( 'NONE',  ( 0.000000000000000000, 0.000000000000000000, -5.324496230895142901 ) ) ;
#28749=CARTESIAN_POINT ( 'NONE',  ( -2.179555516819077443, 4.788648424347429433, -4.057628883416041887 ) ) ;
#28779=LINE ( 'NONE', #11699, #16784 ) ;
#28843=AXIS2_PLACEMENT_3D ( 'NONE', #28187, #34016, #20109 ) ;
#28860=DIRECTION ( 'NONE',  ( 0.000000000000000000, 0.000000000000000000, 1.000000000000000000 ) ) ;
#28878=ORIENTED_EDGE ( 'NONE', *, *, #8363, .T. ) ;
#28919=VERTEX_POINT ( 'NONE', #35111 ) ;
#28938=DIRECTION ( 'NONE',  ( -0.000000000000000000, -0.000000000000000000, 1.000000000000000000 ) ) ;
#28951=DIRECTION ( 'NONE',  ( 1.000000000000000000, 0.000000000000000000, 0.000000000000000000 ) ) ;
#28965=LINE ( 'NONE', #845, #18279 ) ;
#28976=ORIENTED_EDGE ( 'NONE', *, *, #27397, .T. ) ;
#28979=PRODUCT_CONTEXT ( 'NONE', #11542, 'mechanical' ) ;
#28989=MECHANICAL_DESIGN_GEOMETRIC_PRESENTATION_REPRESENTATION('',(#32584),#3844);
#28992=ORIENTED_EDGE ( 'NONE', *, *, #998, .F. ) ;
#29110=DIRECTION ( 'NONE',  ( 0.000000000000000000, 0.000000000000000000, -1.000000000000000000 ) ) ;
#29137=CARTESIAN_POINT ( 'NONE',  ( -5.000000000000001776, -2.068744420501230419, -4.095495254313954447 ) ) ;
#29157=EDGE_LOOP ( 'NONE', ( #35470, #3890, #16862, #22385 ) ) ;
#29162=CARTESIAN_POINT ( 'NONE',  ( 4.451834738187385721E-15, -5.807447148981909280, -4.151008977024224222 ) ) ;
#29174=AXIS2_PLACEMENT_3D ( 'NONE', #4261, #7431, #36121 ) ;
#29177=FACE_OUTER_BOUND ( 'NONE', #8809, .T. ) ;
#29240=FACE_OUTER_BOUND ( 'NONE', #29307, .T. ) ;
#29265=ORIENTED_EDGE ( 'NONE', *, *, #24660, .T. ) ;
#29271=DIRECTION ( 'NONE',  ( 1.000000000000000000, 0.000000000000000000, 0.000000000000000000 ) ) ;
#29307=EDGE_LOOP ( 'NONE', ( #16009, #24700 ) ) ;
#29311=ADVANCED_FACE ( 'NONE', ( #10719 ), #5435, .F. ) ;
#29326=CARTESIAN_POINT ( 'NONE',  ( -5.253687110065723864, -3.069397772387414847, -4.366238859879560508 ) ) ;
#29352=ORIENTED_EDGE ( 'NONE', *, *, #23980, .T. ) ;
#29367=CONICAL_SURFACE ( 'NONE', #14385, 4.999999999999997335, 0.9110539511682894664 ) ;
#29388=FACE_OUTER_BOUND ( 'NONE', #33158, .T. ) ;
#29449=ORIENTED_EDGE ( 'NONE', *, *, #17370, .T. ) ;
#29471=CARTESIAN_POINT ( 'NONE',  ( 2.500000000000021760, -4.330127018922177662, 0.000000000000000000 ) ) ;
#29556=FACE_OUTER_BOUND ( 'NONE', #2610, .T. ) ;
#29651=ORIENTED_EDGE ( 'NONE', *, *, #33732, .F. ) ;
#29670=ORIENTED_EDGE ( 'NONE', *, *, #8035, .T. ) ;
#29671=CONICAL_SURFACE ( 'NONE', #18907, 4.999999999999997335, 0.9110539511682894664 ) ;
#29677=CARTESIAN_POINT ( 'NONE',  ( 3.000000000000000888, 0.000000000000000000, -25.03750572909317285 ) ) ;
#29715=VERTEX_POINT ( 'NONE', #30553 ) ;
#29725=CARTESIAN_POINT ( 'NONE',  ( -5.000000000000000888, -2.886751345948162406, -3.984345921091775100 ) ) ;
#29758=ORIENTED_EDGE ( 'NONE', *, *, #33113, .F. ) ;
#29777=CARTESIAN_POINT ( 'NONE',  ( -3.357433326862113265, 3.835087656846187798, -0.07080520455421240866 ) ) ;
#29794=CARTESIAN_POINT ( 'NONE',  ( -9.999999999999971578, -3.946495907847236140E-14, -5.700000000000000178 ) ) ;
#29834=CIRCLE ( 'NONE', #2303, 6.532899837730827386 ) ;
#29885=CARTESIAN_POINT ( 'NONE',  ( -5.000000000000000888, -3.083558429163938630, -4.289113568008026789 ) ) ;
#29931=PLANE ( 'NONE',  #15880 ) ;
#29950=ORIENTED_EDGE ( 'NONE', *, *, #19934, .T. ) ;
#30030=ADVANCED_FACE ( 'NONE', ( #33823 ), #20774, .T. ) ;
#30035=EDGE_LOOP ( 'NONE', ( #557, #9431, #28878, #34178, #16863 ) ) ;
#30047=ORIENTED_EDGE ( 'NONE', *, *, #14594, .T. ) ;
#30129=CARTESIAN_POINT ( 'NONE',  ( 0.000000000000000000, 0.000000000000000000, 2.266666666666999674 ) ) ;
#30170=EDGE_LOOP ( 'NONE', ( #1874, #17643, #17702 ) ) ;
#30217=CARTESIAN_POINT ( 'NONE',  ( 0.7030283904595543421, -5.367609061415079097, -4.096693167836665594 ) ) ;
#30329=DIRECTION ( 'NONE',  ( -0.000000000000000000, -0.000000000000000000, -1.000000000000000000 ) ) ;
#30346=ORIENTED_EDGE ( 'NONE', *, *, #9835, .T. ) ;
#30384=DIRECTION ( 'NONE',  ( 0.000000000000000000, 0.000000000000000000, 1.000000000000000000 ) ) ;
#30399=CARTESIAN_POINT ( 'NONE',  ( 0.8333333333333367010, -5.292377467571611760, -3.818275046351177870 ) ) ;
#30437=ORIENTED_EDGE ( 'NONE', *, *, #17525, .T. ) ;
#30525=CARTESIAN_POINT ( 'NONE',  ( 4.999999999999999112, 2.886751345948153968, -0.5999999999999998668 ) ) ;
#30544=CARTESIAN_POINT ( 'NONE',  ( -5.854691731421723944E-14, -5.773502691896269745, -0.5999999999999998668 ) ) ;
#30553=CARTESIAN_POINT ( 'NONE',  ( -5.000000000000000888, -2.886751345948150860, -0.5999999999999998668 ) ) ;
#30555=CARTESIAN_POINT ( 'NONE',  ( 1.432312439535579074, 4.946556719366745014, -0.1121614189353384305 ) ) ;
#30580=EDGE_CURVE ( 'NONE', #3218, #23996, #29834, .T. ) ;
#30594=CARTESIAN_POINT ( 'NONE',  ( 4.654160418576254177E-15, -6.066067634115602125, -4.359491423763670603 ) ) ;
#30608=ORIENTED_EDGE ( 'NONE', *, *, #6139, .F. ) ;
#30696=CARTESIAN_POINT ( 'NONE',  ( 5.211749180171790563, 2.764497899775259171, -4.027903350935051030 ) ) ;
#30698=B_SPLINE_CURVE_WITH_KNOTS ( 'NONE', 3,
 ( #20120, #31896, #31548, #26309, #17323, #28749, #620, #3075, #14496, #18217 ),
 .UNSPECIFIED., .F., .F.,
 ( 4, 2, 2, 2, 4 ),
 ( 0.000000000000000000, 0.001528561485809837783, 0.003057122971619675132, 0.004585684457429512265, 0.006114245943239348530 ),
 .UNSPECIFIED. ) ;
#30699=( NAMED_UNIT ( * ) PLANE_ANGLE_UNIT ( ) SI_UNIT ( $, .RADIAN. ) );
#30759=CARTESIAN_POINT ( 'NONE',  ( 4.999999999999999112, -2.119101676855895899, -3.842106124101172249 ) ) ;
#30772=CARTESIAN_POINT ( 'NONE',  ( -5.211749180171789675, 2.764497899775240519, -4.027903350935047477 ) ) ;
#30773=FACE_OUTER_BOUND ( 'NONE', #24480, .T. ) ;
#30776=ORIENTED_EDGE ( 'NONE', *, *, #27061, .T. ) ;
#30790=CARTESIAN_POINT ( 'NONE',  ( 0.000000000000000000, 3.050000000000000711, 2.266666666666999674 ) ) ;
#30791=CARTESIAN_POINT ( 'NONE',  ( -5.244818697407747976, 2.029379090245544415, -4.190884354498993325 ) ) ;
#30831=B_SPLINE_CURVE_WITH_KNOTS ( 'NONE', 3,
 ( #34982, #11913, #29162, #14728, #34808, #9280 ),
 .UNSPECIFIED., .F., .F.,
 ( 4, 2, 4 ),
 ( 0.000000000000000000, 0.0002514304509865748229, 0.0005028609019731496458 ),
 .UNSPECIFIED. ) ;
#30843=CARTESIAN_POINT ( 'NONE',  ( 5.253368672218635460, -3.033033817057790404, -4.359491423763655504 ) ) ;
#30871=VERTEX_POINT ( 'NONE', #35827 ) ;
#30878=CARTESIAN_POINT ( 'NONE',  ( 0.6806757771963801718, 5.380514348701075811, -3.838711833384166550 ) ) ;
#30906=CARTESIAN_POINT ( 'NONE',  ( -5.253368672218638125, -3.033033817057809500, -4.359491423763659945 ) ) ;
#30954=CLOSED_SHELL ( 'NONE', ( #14090, #27677, #18133, #24508, #33502, #4683, #27904, #30030, #17937, #2227, #5506, #28150, #7396, #21571, #20420, #25322, #24249, #3399, #8676, #6891, #36879, #2858, #7871, #20897, #8664, #13961, #3125, #16230, #29311, #34667, #10663, #4237, #27724, #18520, #22167, #24318, #28115, #4370, #36166 ) ) ;
#30971=CARTESIAN_POINT ( 'NONE',  ( 5.284804376168104056, -3.015249596956828704, -4.366192694417983411 ) ) ;
#31041=DIRECTION ( 'NONE',  ( -0.000000000000000000, -0.000000000000000000, 1.000000000000000000 ) ) ;
#31045=ORIENTED_EDGE ( 'NONE', *, *, #21119, .T. ) ;
#31051=( BOUNDED_SURFACE ( )  B_SPLINE_SURFACE ( 3, 2, ( 
 ( #30696, #33710, #36153 ),
 ( #16454, #5211, #22272 ),
 ( #10455, #17348, #3094 ),
 ( #21898, #19455, #24548 ),
 ( #30878, #7461, #33343 ),
 ( #16651, #28583, #35984 ) ),
 .UNSPECIFIED., .F., .F., .F. ) 
 B_SPLINE_SURFACE_WITH_KNOTS ( ( 4, 2, 4 ),
 ( 3, 3 ),
 ( 0.002450104044831664246, 0.005591829551853650000, 0.008733555058875635754 ),
 ( 0.000000000000000000, 1.000000000000000000 ),
 .UNSPECIFIED. ) 
 GEOMETRIC_REPRESENTATION_ITEM ( )  RATIONAL_B_SPLINE_SURFACE ( (
 ( 1.000000000000000000, 0.8047731410850403888, 1.000000000000000000),
 ( 1.000000000000000000, 0.8125552299154461533, 1.000000000000000000),
 ( 1.000000000000000000, 0.8191520442892223919, 1.000000000000000000),
 ( 1.000000000000000000, 0.8191520442887518794, 1.000000000000000000),
 ( 1.000000000000000000, 0.8125552299157995373, 1.000000000000000000),
 ( 1.000000000000000000, 0.8047731410850398337, 1.000000000000000000) ) ) 
 REPRESENTATION_ITEM ( '' )  SURFACE ( )  );
#31160=CARTESIAN_POINT ( 'NONE',  ( -6.726859516510129033, 8.238026975208041383E-16, -4.599999999999999645 ) ) ;
#31204=FACE_OUTER_BOUND ( 'NONE', #25702, .T. ) ;
#31235=CARTESIAN_POINT ( 'NONE',  ( 0.4022569922705656609, -5.541259509125485039, -0.4198507760575983516 ) ) ;
#31249=DIRECTION ( 'NONE',  ( 1.000000000000000000, 0.000000000000000000, 0.000000000000000000 ) ) ;
#31313=CARTESIAN_POINT ( 'NONE',  ( -4.817183509279844955, -3.279805190042336616, -4.266911319714225215 ) ) ;
#31322=CARTESIAN_POINT ( 'NONE',  ( -1.582370436568139027, 4.859920694385941431, -3.719399823475518119 ) ) ;
#31345=CARTESIAN_POINT ( 'NONE',  ( 2.500000000000008438, 4.330127018922190096, -2.691222917490924395E-15 ) ) ;
#31354=EDGE_CURVE ( 'NONE', #15333, #36697, #12171, .T. ) ;
#31385=AXIS2_PLACEMENT_3D ( 'NONE', #19697, #16706, #27940 ) ;
#31407=EDGE_CURVE ( 'NONE', #33059, #8160, #5819, .T. ) ;
#31421=AXIS2_PLACEMENT_3D ( 'NONE', #91, #31041, #5719 ) ;
#31435=AXIS2_PLACEMENT_3D ( 'NONE', #24711, #5398, #13636 ) ;
#31449=CARTESIAN_POINT ( 'NONE',  ( -2.930059260563453005, -4.081832189068429706, -2.862547845245907365E-14 ) ) ;
#31453=CONICAL_SURFACE ( 'NONE', #34474, 3.000000000000000888, 0.9599310885968804774 ) ;
#31497=CYLINDRICAL_SURFACE ( 'NONE', #18988, 3.000000000000000888 ) ;
#31525=ORIENTED_EDGE ( 'NONE', *, *, #19867, .F. ) ;
#31543=DIRECTION ( 'NONE',  ( 0.000000000000000000, 0.000000000000000000, 1.000000000000000000 ) ) ;
#31548=CARTESIAN_POINT ( 'NONE',  ( -4.378301941662551044, 3.528365556573270556, -4.190643565754935906 ) ) ;
#31560=EDGE_CURVE ( 'NONE', #22867, #18257, #30831, .T. ) ;
#31574=EDGE_CURVE ( 'NONE', #36512, #33080, #11017, .T. ) ;
#31587=AXIS2_PLACEMENT_3D ( 'NONE', #33694, #36522, #19265 ) ;
#31590=CARTESIAN_POINT ( 'NONE',  ( -5.238704763094644612, -1.015773027556931440, -4.085839086323462155 ) ) ;
#31591=MANIFOLD_SOLID_BREP ( 'TorqueElement', #30954 ) ;
#31687=CARTESIAN_POINT ( 'NONE',  ( -0.4317663827706223478, -5.811727376006694534, -4.266919140436448821 ) ) ;
#31701=AXIS2_PLACEMENT_3D ( 'NONE', #28622, #33887, #31249 ) ;
#31704=FACE_OUTER_BOUND ( 'NONE', #15206, .T. ) ;
#31716=DIRECTION ( 'NONE',  ( -0.8660254037844360431, -0.5000000000000045519, 0.000000000000000000 ) ) ;
#31719=VERTEX_POINT ( 'NONE', #11080 ) ;
#31741=DIRECTION ( 'NONE',  ( -1.000000000000000000, 0.000000000000000000, 0.000000000000000000 ) ) ;
#31774=CARTESIAN_POINT ( 'NONE',  ( 0.4317663827706206270, 5.811727376006657231, -4.266919140436438163 ) ) ;
#31782=FILL_AREA_STYLE ('',( #17374 ) ) ;
#31833=ORIENTED_EDGE ( 'NONE', *, *, #31560, .F. ) ;
#31851=ORIENTED_EDGE ( 'NONE', *, *, #27069, .T. ) ;
#31866=CARTESIAN_POINT ( 'NONE',  ( -5.000000000000000888, 2.886751345948107783, -0.5999999999999836575 ) ) ;
#31877=CARTESIAN_POINT ( 'NONE',  ( -3.750000000000001776, 4.592425496802576930E-16, 2.266666666666999674 ) ) ;
#31879=ORIENTED_EDGE ( 'NONE', *, *, #20519, .F. ) ;
#31896=CARTESIAN_POINT ( 'NONE',  ( -4.817220356105919699, 3.279784343982782957, -4.266919140436429281 ) ) ;
#31911=EDGE_CURVE ( 'NONE', #11174, #33080, #9184, .T. ) ;
#31961=CARTESIAN_POINT ( 'NONE',  ( 0.000000000000000000, 0.000000000000000000, 13.31572692736085095 ) ) ;
#31963=DIRECTION ( 'NONE',  ( -1.000000000000000000, 0.000000000000000000, 0.000000000000000000 ) ) ;
#32005=( NAMED_UNIT ( * ) PLANE_ANGLE_UNIT ( ) SI_UNIT ( $, .RADIAN. ) );
#32035=FACE_OUTER_BOUND ( 'NONE', #3812, .T. ) ;
#32053=CARTESIAN_POINT ( 'NONE',  ( 5.236872748402764621, 8.442024233997350580E-14, -4.057689166958447835 ) ) ;
#32067=DIRECTION ( 'NONE',  ( -0.5000000000000045519, 0.8660254037844360431, 0.000000000000000000 ) ) ;
#32076=CARTESIAN_POINT ( 'NONE',  ( -6.069707180676227632E-15, 5.773502691896268857, -3.984345921091771547 ) ) ;
#32086=ORIENTED_EDGE ( 'NONE', *, *, #15598, .F. ) ;
#32089=COLOUR_RGB ( '', 0.09019608, 0.27058824, 0.51372549) ;
#32125=CARTESIAN_POINT ( 'NONE',  ( -5.000000000000000888, 1.087997039530374854, -3.720971761088881280 ) ) ;
#32163=CIRCLE ( 'NONE', #20214, 3.000000000000000888 ) ;
#32238=ORIENTED_EDGE ( 'NONE', *, *, #36236, .F. ) ;
#32240=( BOUNDED_SURFACE ( )  B_SPLINE_SURFACE ( 3, 2, ( 
 ( #8468, #19537, #30772 ),
 ( #10903, #11453, #2479 ),
 ( #25345, #36610, #33984 ),
 ( #36779, #19184, #31322 ),
 ( #17082, #22900, #5301 ),
 ( #14077, #22343, #16737 ) ),
 .UNSPECIFIED., .F., .F., .F. ) 
 B_SPLINE_SURFACE_WITH_KNOTS ( ( 4, 2, 4 ),
 ( 3, 3 ),
 ( 0.002450104044831661210, 0.005591829551853644796, 0.008733555058875628815 ),
 ( 0.000000000000000000, 1.000000000000000000 ),
 .UNSPECIFIED. ) 
 GEOMETRIC_REPRESENTATION_ITEM ( )  RATIONAL_B_SPLINE_SURFACE ( (
 ( 1.000000000000000000, 0.8047731410850402778, 1.000000000000000000),
 ( 1.000000000000000000, 0.8125552299159768399, 1.000000000000000000),
 ( 1.000000000000000000, 0.8191520442885167341, 1.000000000000000000),
 ( 1.000000000000000000, 0.8191520442894577592, 1.000000000000000000),
 ( 1.000000000000000000, 0.8125552299152696278, 1.000000000000000000),
 ( 1.000000000000000000, 0.8047731410850398337, 1.000000000000000000) ) ) 
 REPRESENTATION_ITEM ( '' )  SURFACE ( )  );
#32261=VERTEX_POINT ( 'NONE', #28285 ) ;
#32263=EDGE_CURVE ( 'NONE', #36034, #35959, #25855, .T. ) ;
#32327=CARTESIAN_POINT ( 'NONE',  ( -5.244935714621999701, 2.071324742674405694, -4.180276246144004837 ) ) ;
#32376=FACE_OUTER_BOUND ( 'NONE', #4542, .T. ) ;
#32387=DIRECTION ( 'NONE',  ( 1.000000000000000000, 0.000000000000000000, 0.000000000000000000 ) ) ;
#32398=CARTESIAN_POINT ( 'NONE',  ( -4.400655246573610846, -3.515428273945304216, -4.176900509772398351 ) ) ;
#32436=EDGE_CURVE ( 'NONE', #8160, #27610, #6198, .T. ) ;
#32455=ORIENTED_EDGE ( 'NONE', *, *, #25254, .T. ) ;
#32533=CIRCLE ( 'NONE', #18162, 3.750000000000001776 ) ;
#32584=STYLED_ITEM ( 'NONE', ( #3672 ), #31591 ) ;
#32671=EDGE_CURVE ( 'NONE', #35959, #32911, #28464, .T. ) ;
#32688=EDGE_CURVE ( 'NONE', #17855, #35211, #280, .T. ) ;
#32699=AXIS2_PLACEMENT_3D ( 'NONE', #12250, #23534, #6662 ) ;
#32738=DIRECTION ( 'NONE',  ( 0.5000000000000045519, -0.8660254037844360431, 0.000000000000000000 ) ) ;
#32760=EDGE_CURVE ( 'NONE', #8805, #14671, #35716, .T. ) ;
#32763=DIRECTION ( 'NONE',  ( 1.000000000000000000, 0.000000000000000000, 0.000000000000000000 ) ) ;
#32789=CARTESIAN_POINT ( 'NONE',  ( -2.500000000000022204, 4.330127018922177662, 0.000000000000000000 ) ) ;
#32807=FACE_OUTER_BOUND ( 'NONE', #30035, .T. ) ;
#32826=UNCERTAINTY_MEASURE_WITH_UNIT (LENGTH_MEASURE( 1.000000000000000082E-05 ), #26416, 'distance_accuracy_value', 'NONE');
#32854=CARTESIAN_POINT ( 'NONE',  ( 0.000000000000000000, 0.000000000000000000, 2.266666666667000563 ) ) ;
#32911=VERTEX_POINT ( 'NONE', #4402 ) ;
#32926=CARTESIAN_POINT ( 'NONE',  ( 4.390739357591696154E-15, -5.773502691896305272, -5.700000000000000178 ) ) ;
#32929=FACE_OUTER_BOUND ( 'NONE', #23731, .T. ) ;
#32951=DIRECTION ( 'NONE',  ( -0.000000000000000000, -0.000000000000000000, 1.000000000000000000 ) ) ;
#32966=CARTESIAN_POINT ( 'NONE',  ( 0.1702248550645389935, -5.871782057790579934, -4.289066185948700038 ) ) ;
#32975=EDGE_CURVE ( 'NONE', #29715, #34191, #12827, .T. ) ;
#32989=ORIENTED_EDGE ( 'NONE', *, *, #17155, .F. ) ;
#33010=EDGE_LOOP ( 'NONE', ( #33359, #24033 ) ) ;
#33032=ORIENTED_EDGE ( 'NONE', *, *, #6043, .T. ) ;
#33033=DIRECTION ( 'NONE',  ( 0.000000000000000000, 0.000000000000000000, -1.000000000000000000 ) ) ;
#33046=CARTESIAN_POINT ( 'NONE',  ( -6.532899837730827386, 8.119260925317680943E-16, -5.700000000000001066 ) ) ;
#33059=VERTEX_POINT ( 'NONE', #26113 ) ;
#33064=CARTESIAN_POINT ( 'NONE',  ( -5.238715782502663565, 1.018209582082210352, -4.086015505371660694 ) ) ;
#33074=DIRECTION ( 'NONE',  ( 0.000000000000000000, 0.000000000000000000, 1.000000000000000000 ) ) ;
#33080=VERTEX_POINT ( 'NONE', #11495 ) ;
#33113=EDGE_CURVE ( 'NONE', #23645, #16885, #35120, .T. ) ;
#33158=EDGE_LOOP ( 'NONE', ( #29651, #28976, #33177, #20610, #30437, #2702, #11534 ) ) ;
#33161=CARTESIAN_POINT ( 'NONE',  ( 0.000000000000000000, 0.000000000000000000, 2.266666666666999674 ) ) ;
#33172=EDGE_CURVE ( 'NONE', #15802, #17855, #30698, .T. ) ;
#33177=ORIENTED_EDGE ( 'NONE', *, *, #15358, .T. ) ;
#33178=UNCERTAINTY_MEASURE_WITH_UNIT (LENGTH_MEASURE( 1.000000000000000082E-05 ), #285, 'distance_accuracy_value', 'NONE');
#33210=ORIENTED_EDGE ( 'NONE', *, *, #36645, .T. ) ;
#33235=EDGE_CURVE ( 'NONE', #23645, #36034, #21218, .T. ) ;
#33337=CARTESIAN_POINT ( 'NONE',  ( -3.401922400365994026, -3.809401878283186882, -3.971474537230573532 ) ) ;
#33343=CARTESIAN_POINT ( 'NONE',  ( 0.8441225671308623113, 5.568793373801118385, -4.176900509771833470 ) ) ;
#33359=ORIENTED_EDGE ( 'NONE', *, *, #35360, .T. ) ;
#33371=CARTESIAN_POINT ( 'NONE',  ( -1.074820392479180450E-14, 5.987020429981924075, -4.330720594357048370 ) ) ;
#33502=ADVANCED_FACE ( 'NONE', ( #32035 ), #31497, .F. ) ;
#33615=CARTESIAN_POINT ( 'NONE',  ( 1.721886139903932023, -5.052888355616823368, -4.057689166958430960 ) ) ;
#33643=CARTESIAN_POINT ( 'NONE',  ( 5.253368672218635460, -3.033033817057790404, -4.359491423763655504 ) ) ;
#33668=CIRCLE ( 'NONE', #1323, 5.000000000000000000 ) ;
#33687=CARTESIAN_POINT ( 'NONE',  ( 0.000000000000000000, 0.000000000000000000, 3.400000000000000355 ) ) ;
#33694=CARTESIAN_POINT ( 'NONE',  ( 0.000000000000000000, 0.000000000000000000, 0.000000000000000000 ) ) ;
#33710=CARTESIAN_POINT ( 'NONE',  ( 5.170224855064532221, 2.788471980053852217, -4.289066185948682275 ) ) ;
#33732=EDGE_CURVE ( 'NONE', #9870, #16004, #2599, .T. ) ;
#33741=CARTESIAN_POINT ( 'NONE',  ( -6.216324218022825094E-15, 6.066067634115565710, -4.359491423763658169 ) ) ;
#33754=CARTESIAN_POINT ( 'NONE',  ( -6.726859516510129922, 0.000000000000000000, -4.599999999999999645 ) ) ;
#33758=AXIS2_PLACEMENT_3D ( 'NONE', #22626, #33876, #5000 ) ;
#33795=DIRECTION ( 'NONE',  ( -0.000000000000000000, -0.000000000000000000, 1.000000000000000000 ) ) ;
#33807=CARTESIAN_POINT ( 'NONE',  ( 4.185558440016312609, 3.356969399843928059, -0.2680587191991100071 ) ) ;
#33823=FACE_OUTER_BOUND ( 'NONE', #7337, .T. ) ;
#33829=AXIS2_PLACEMENT_3D ( 'NONE', #7128, #10129, #21562 ) ;
#33845=EDGE_CURVE ( 'NONE', #17855, #30871, #25331, .T. ) ;
#33876=DIRECTION ( 'NONE',  ( -0.000000000000000000, -0.000000000000000000, 1.000000000000000000 ) ) ;
#33887=DIRECTION ( 'NONE',  ( -0.000000000000000000, -0.000000000000000000, 1.000000000000000000 ) ) ;
#33925=DIRECTION ( 'NONE',  ( 0.9396926207859139790, 1.150791560227857172E-16, -0.3420201433256533918 ) ) ;
#33935=UNCERTAINTY_MEASURE_WITH_UNIT (LENGTH_MEASURE( 1.000000000000000082E-05 ), #21900, 'distance_accuracy_value', 'NONE');
#33970=DIRECTION ( 'NONE',  ( -0.000000000000000000, -0.000000000000000000, 1.000000000000000000 ) ) ;
#33984=CARTESIAN_POINT ( 'NONE',  ( -3.417629563431864526, 3.800333343458438762, -3.719399823475518119 ) ) ;
#33992=FACE_OUTER_BOUND ( 'NONE', #17501, .T. ) ;
#34016=DIRECTION ( 'NONE',  ( 0.000000000000000000, 0.000000000000000000, 1.000000000000000000 ) ) ;
#34021=PRODUCT ( 'torque nut 04-2_iso_ISO 7043-M6-N', 'torque nut 04-2_iso_ISO 7043-M6-N', '', ( #28979 ) ) ;
#34178=ORIENTED_EDGE ( 'NONE', *, *, #16633, .T. ) ;
#34185=VERTEX_POINT ( 'NONE', #35546 ) ;
#34191=VERTEX_POINT ( 'NONE', #21274 ) ;
#34215=CARTESIAN_POINT ( 'NONE',  ( 0.000000000000000000, 0.000000000000000000, -5.132899837730832360 ) ) ;
#34247=CARTESIAN_POINT ( 'NONE',  ( -5.248984340851196251, -2.531668808681923899, -4.266868479993930485 ) ) ;
#34249=B_SPLINE_CURVE_WITH_KNOTS ( 'NONE', 3,
 ( #34372, #17124, #25571, #6060, #2888 ),
 .UNSPECIFIED., .F., .F.,
 ( 4, 1, 4 ),
 ( 0.000000000000000000, 0.002886751345948135490, 0.005773502691896270980 ),
 .UNSPECIFIED. ) ;
#34290=ORIENTED_EDGE ( 'NONE', *, *, #35574, .T. ) ;
#34327=CARTESIAN_POINT ( 'NONE',  ( -5.253368672218638125, -3.033033817057809500, -4.359491423763659945 ) ) ;
#34357=ORIENTED_EDGE ( 'NONE', *, *, #18505, .F. ) ;
#34372=CARTESIAN_POINT ( 'NONE',  ( 4.999999999999999112, -2.886751345948144198, -3.984345921091770659 ) ) ;
#34376=CARTESIAN_POINT ( 'NONE',  ( 3.000000000000000888, 3.673940397442060854E-16, -5.674599999999998090 ) ) ;
#34404=ORIENTED_EDGE ( 'NONE', *, *, #31574, .F. ) ;
#34443=SHAPE_REPRESENTATION ( 'torque nut 04-2_iso_ISO 7043-M6-N', ( #21385 ), #11148 ) ;
#34447=EDGE_CURVE ( 'NONE', #33059, #14671, #19039, .T. ) ;
#34474=AXIS2_PLACEMENT_3D ( 'NONE', #8308, #19733, #22908 ) ;
#34475=CARTESIAN_POINT ( 'NONE',  ( -5.000000000000000888, 2.119000125145918734, -3.842087316602514679 ) ) ;
#34483=AXIS2_PLACEMENT_3D ( 'NONE', #882, #26398, #1263 ) ;
#34511=CARTESIAN_POINT ( 'NONE',  ( -0.8665032349992070060, -5.555903485205192283, -4.190643565754955446 ) ) ;
#34536=EDGE_LOOP ( 'NONE', ( #1651, #19126 ) ) ;
#34581=DIRECTION ( 'NONE',  ( 0.000000000000000000, 0.000000000000000000, 1.000000000000000000 ) ) ;
#34600=DIRECTION ( 'NONE',  ( 1.000000000000000000, 0.000000000000000000, 0.000000000000000000 ) ) ;
#34628=( NAMED_UNIT ( * ) SI_UNIT ( $, .STERADIAN. ) SOLID_ANGLE_UNIT ( ) );
#34638=AXIS2_PLACEMENT_3D ( 'NONE', #29794, #20800, #23612 ) ;
#34661=ORIENTED_EDGE ( 'NONE', *, *, #5268, .T. ) ;
#34664=CIRCLE ( 'NONE', #26890, 3.000000000000000888 ) ;
#34667=ADVANCED_FACE ( 'NONE', ( #2647 ), #32240, .F. ) ;
#34698=ORIENTED_EDGE ( 'NONE', *, *, #31560, .T. ) ;
#34714=VERTEX_POINT ( 'NONE', #31160 ) ;
#34768=CARTESIAN_POINT ( 'NONE',  ( 0.000000000000000000, 0.000000000000000000, 0.000000000000000000 ) ) ;
#34801=CARTESIAN_POINT ( 'NONE',  ( -6.216324218022825094E-15, 6.066067634115565710, -4.359491423763658169 ) ) ;
#34808=CARTESIAN_POINT ( 'NONE',  ( -6.912404044025940083E-14, -5.987311224403031318, -4.330826434870623132 ) ) ;
#34874=CARTESIAN_POINT ( 'NONE',  ( 0.000000000000000000, 0.000000000000000000, 0.000000000000000000 ) ) ;
#34892=CONICAL_SURFACE ( 'NONE', #19342, 3.050000000000000711, 0.7853981633974498333 ) ;
#34982=CARTESIAN_POINT ( 'NONE',  ( 4.390739357591696154E-15, -5.773502691896305272, -3.984345921091785758 ) ) ;
#35028=CARTESIAN_POINT ( 'NONE',  ( 5.253368672218635460, 3.033033817057773529, -4.359491423763652840 ) ) ;
#35064=DIRECTION ( 'NONE',  ( -1.000000000000000000, 0.000000000000000000, 0.000000000000000000 ) ) ;
#35071=ORIENTED_EDGE ( 'NONE', *, *, #17370, .F. ) ;
#35073=ORIENTED_EDGE ( 'NONE', *, *, #9110, .F. ) ;
#35093=CIRCLE ( 'NONE', #6957, 2.500000000000000444 ) ;
#35111=CARTESIAN_POINT ( 'NONE',  ( -2.500000000000000444, 3.061616997868383634E-16, -5.324496230895142901 ) ) ;
#35120=LINE ( 'NONE', #34376, #6983 ) ;
#35154=CARTESIAN_POINT ( 'NONE',  ( 5.185163620696106257, 2.993655612202505090, -4.330826434870604480 ) ) ;
#35175=CARTESIAN_POINT ( 'NONE',  ( 4.817183509279844955, 3.279805190042301533, -4.266911319714219886 ) ) ;
#35186=CARTESIAN_POINT ( 'NONE',  ( -1.647413659512548589, 4.822367972110025214, -0.05822226285683017311 ) ) ;
#35211=VERTEX_POINT ( 'NONE', #35028 ) ;
#35212=B_SPLINE_CURVE_WITH_KNOTS ( 'NONE', 3,
 ( #17706, #34247, #20508, #31590, #5929, #13972 ),
 .UNSPECIFIED., .F., .F.,
 ( 4, 2, 4 ),
 ( 0.000000000000000000, 0.001529397995383628651, 0.003058795990767257302 ),
 .UNSPECIFIED. ) ;
#35239=CARTESIAN_POINT ( 'NONE',  ( -4.319324222803747837, -3.279739689143278181, -3.838711833383472438 ) ) ;
#35354=CARTESIAN_POINT ( 'NONE',  ( 4.999999999999999112, 2.886751345948126879, -4.069522543421416394 ) ) ;
#35359=DIRECTION ( 'NONE',  ( -0.000000000000000000, -0.000000000000000000, 1.000000000000000000 ) ) ;
#35360=EDGE_CURVE ( 'NONE', #21285, #11174, #32533, .T. ) ;
#35390=ORIENTED_EDGE ( 'NONE', *, *, #9835, .F. ) ;
#35453=CARTESIAN_POINT ( 'NONE',  ( -5.204170427930421283E-15, 5.773502691896269745, -0.5999999999999998668 ) ) ;
#35470=ORIENTED_EDGE ( 'NONE', *, *, #24733, .F. ) ;
#35546=CARTESIAN_POINT ( 'NONE',  ( 5.253368672218635460, -3.033033817057790404, -4.359491423763655504 ) ) ;
#35567=CIRCLE ( 'NONE', #27162, 4.999999999999997335 ) ;
#35574=EDGE_CURVE ( 'NONE', #16885, #24399, #5112, .T. ) ;
#35659=CARTESIAN_POINT ( 'NONE',  ( -5.000000000000000888, -2.886751345948162406, -3.984345921091775100 ) ) ;
#35688=ORIENTED_EDGE ( 'NONE', *, *, #36156, .F. ) ;
#35712=AXIS2_PLACEMENT_3D ( 'NONE', #3704, #32951, #32387 ) ;
#35716=CIRCLE ( 'NONE', #32699, 4.999999999999997335 ) ;
#35824=DIRECTION ( 'NONE',  ( -1.000000000000000000, 0.000000000000000000, -0.000000000000000000 ) ) ;
#35827=CARTESIAN_POINT ( 'NONE',  ( -6.069707180676227632E-15, 5.773502691896268857, -3.984345921091771547 ) ) ;
#35867=VECTOR ( 'NONE', #1011, 1000.000000000000000 ) ;
#35894=ORIENTED_EDGE ( 'NONE', *, *, #13222, .T. ) ;
#35900=ORIENTED_EDGE ( 'NONE', *, *, #24660, .F. ) ;
#35959=VERTEX_POINT ( 'NONE', #3047 ) ;
#35975=CARTESIAN_POINT ( 'NONE',  ( 5.000000000000000000, 0.9888715124523291822, -0.07061148569344767589 ) ) ;
#35984=CARTESIAN_POINT ( 'NONE',  ( -0.03111943836866844226, 6.084399642271172581, -4.366192694417985187 ) ) ;
#36034=VERTEX_POINT ( 'NONE', #27475 ) ;
#36081=CARTESIAN_POINT ( 'NONE',  ( 0.000000000000000000, 0.000000000000000000, 3.400000000000000355 ) ) ;
#36093=( BOUNDED_SURFACE ( )  B_SPLINE_SURFACE ( 3, 2, ( 
 ( #30971, #1917, #13341 ),
 ( #24991, #19351, #21783 ),
 ( #10905, #5098, #5302 ),
 ( #33615, #24799, #25186 ),
 ( #16541, #30217, #4920 ),
 ( #27971, #2293, #36611 ) ),
 .UNSPECIFIED., .F., .F., .F. ) 
 B_SPLINE_SURFACE_WITH_KNOTS ( ( 4, 2, 4 ),
 ( 3, 3 ),
 ( 0.002450104044831694170, 0.005591829551853678623, 0.008733555058875663510 ),
 ( 0.000000000000000000, 1.000000000000000000 ),
 .UNSPECIFIED. ) 
 GEOMETRIC_REPRESENTATION_ITEM ( )  RATIONAL_B_SPLINE_SURFACE ( (
 ( 1.000000000000000000, 0.8047731410850409439, 1.000000000000000000),
 ( 1.000000000000000000, 0.8125552299156232339, 1.000000000000000000),
 ( 1.000000000000000000, 0.8191520442889870246, 1.000000000000000000),
 ( 1.000000000000000000, 0.8191520442889870246, 1.000000000000000000),
 ( 1.000000000000000000, 0.8125552299156219016, 1.000000000000000000),
 ( 1.000000000000000000, 0.8047731410850398337, 1.000000000000000000) ) ) 
 REPRESENTATION_ITEM ( '' )  SURFACE ( )  );
#36108=DIRECTION ( 'NONE',  ( 0.000000000000000000, 0.000000000000000000, 1.000000000000000000 ) ) ;
#36121=DIRECTION ( 'NONE',  ( 1.000000000000000000, 0.000000000000000000, 0.000000000000000000 ) ) ;
#36129=CARTESIAN_POINT ( 'NONE',  ( 3.750000000000001776, 0.000000000000000000, 3.400000000000000355 ) ) ;
#36138=CIRCLE ( 'NONE', #6167, 4.999999999999997335 ) ;
#36143=CARTESIAN_POINT ( 'NONE',  ( 4.999999999999997335, 0.000000000000000000, 0.000000000000000000 ) ) ;
#36153=CARTESIAN_POINT ( 'NONE',  ( 5.284804376168104945, 3.015249596956811384, -4.366192694417979858 ) ) ;
#36155=FILL_AREA_STYLE_COLOUR ( '', #32089 ) ;
#36156=EDGE_CURVE ( 'NONE', #34191, #16233, #25595, .T. ) ;
#36166=ADVANCED_FACE ( 'NONE', ( #31704 ), #14467, .T. ) ;
#36236=EDGE_CURVE ( 'NONE', #14671, #8160, #3954, .T. ) ;
#36237=VECTOR ( 'NONE', #28860, 1000.000000000000000 ) ;
#36313=( BOUNDED_SURFACE ( )  B_SPLINE_SURFACE ( 3, 2, ( 
 ( #26580, #893, #12314 ),
 ( #35239, #20970, #32398 ),
 ( #15334, #33337, #4660 ),
 ( #7453, #18712, #16448 ),
 ( #13083, #22092, #27329 ),
 ( #7844, #32966, #24540 ) ),
 .UNSPECIFIED., .F., .F., .T. ) 
 B_SPLINE_SURFACE_WITH_KNOTS ( ( 4, 2, 4 ),
 ( 3, 3 ),
 ( 0.002450104044831698507, 0.005591829551853683827, 0.008733555058875668714 ),
 ( 0.000000000000000000, 1.000000000000000000 ),
 .UNSPECIFIED. ) 
 GEOMETRIC_REPRESENTATION_ITEM ( )  RATIONAL_B_SPLINE_SURFACE ( (
 ( 1.000000000000000000, 0.8047731410850408329, 1.000000000000000000),
 ( 1.000000000000000000, 0.8125552299152700719, 1.000000000000000000),
 ( 1.000000000000000000, 0.8191520442894577592, 1.000000000000000000),
 ( 1.000000000000000000, 0.8191520442885167341, 1.000000000000000000),
 ( 1.000000000000000000, 0.8125552299159767289, 1.000000000000000000),
 ( 1.000000000000000000, 0.8047731410850399447, 1.000000000000000000) ) ) 
 REPRESENTATION_ITEM ( '' )  SURFACE ( )  );
#36318=DIRECTION ( 'NONE',  ( 0.000000000000000000, 0.000000000000000000, 1.000000000000000000 ) ) ;
#36396=DIRECTION ( 'NONE',  ( 1.000000000000000000, 0.000000000000000000, 0.000000000000000000 ) ) ;
#36411=CARTESIAN_POINT ( 'NONE',  ( 4.390739357591696154E-15, -5.773502691896305272, -3.984345921091785758 ) ) ;
#36414=DIRECTION ( 'NONE',  ( -0.7071067811865486830, 8.659560562354947649E-17, 0.7071067811865464625 ) ) ;
#36459=CARTESIAN_POINT ( 'NONE',  ( 5.248988766908545323, -2.532174945215652340, -4.266961984436639099 ) ) ;
#36473=EDGE_LOOP ( 'NONE', ( #13737, #23808, #31525 ) ) ;
#36489=EDGE_CURVE ( 'NONE', #18239, #16233, #13416, .T. ) ;
#36491=CARTESIAN_POINT ( 'NONE',  ( 3.499999647538293512, -4.028415724610473703, -4.085927688751840314 ) ) ;
#36512=VERTEX_POINT ( 'NONE', #36129 ) ;
#36522=DIRECTION ( 'NONE',  ( -0.000000000000000000, -0.000000000000000000, 1.000000000000000000 ) ) ;
#36547=ORIENTED_EDGE ( 'NONE', *, *, #33235, .T. ) ;
#36564=CARTESIAN_POINT ( 'NONE',  ( -5.321755965770424296E-15, 5.914763229585211946, -4.281769937709103857 ) ) ;
#36610=CARTESIAN_POINT ( 'NONE',  ( -3.401922400366804045, 3.809401878282542064, -3.971474537231016733 ) ) ;
#36611=CARTESIAN_POINT ( 'NONE',  ( -0.2117491801717885924, -5.895756138069174312, -4.027903350935069682 ) ) ;
#36612=CARTESIAN_POINT ( 'NONE',  ( -1.642566673137934696, -4.825166380998203053, -0.07080520455423977566 ) ) ;
#36645=EDGE_CURVE ( 'NONE', #14671, #16872, #20617, .T. ) ;
#36664=EDGE_LOOP ( 'NONE', ( #4425, #37065, #31833, #10644 ) ) ;
#36666=EDGE_CURVE ( 'NONE', #36697, #15333, #15985, .T. ) ;
#36697=VERTEX_POINT ( 'NONE', #8182 ) ;
#36727=CARTESIAN_POINT ( 'NONE',  ( 1.642566673137904498, 4.825166380998184401, -0.07080520455421732140 ) ) ;
#36735=VERTEX_POINT ( 'NONE', #29725 ) ;
#36773=DIRECTION ( 'NONE',  ( 1.000000000000000000, 0.000000000000000000, 0.000000000000000000 ) ) ;
#36779=CARTESIAN_POINT ( 'NONE',  ( -1.721886139904403201, 5.052888355616344640, -4.057689166958363458 ) ) ;
#36879=ADVANCED_FACE ( 'NONE', ( #32929 ), #2846, .T. ) ;
#36911=CARTESIAN_POINT ( 'NONE',  ( -4.185558440016324155, -3.356969399843958257, -0.2680587191991318785 ) ) ;
#36940=AXIS2_PLACEMENT_3D ( 'NONE', #33687, #13815, #11169 ) ;
#37009=CARTESIAN_POINT ( 'NONE',  ( 5.244818697407745312, -2.029379090245567951, -4.190884354498995101 ) ) ;
#37018=CARTESIAN_POINT ( 'NONE',  ( -5.000000000000000000, -0.9835753746177081647, -0.05800540215399103972 ) ) ;
#37065=ORIENTED_EDGE ( 'NONE', *, *, #8068, .F. ) ;
#37078=CONICAL_SURFACE ( 'NONE', #28073, 3.000000000000000888, 0.9599310885968804774 ) ;
#37107=ORIENTED_EDGE ( 'NONE', *, *, #33172, .F. ) ;
ENDSEC;
END-ISO-10303-21;
